ISO-10303-21;
HEADER;
/* Generated by software containing ST-Developer
 * from STEP Tools, Inc. (www.steptools.com) 
 */

FILE_DESCRIPTION(
/* description */ (''),
/* implementation_level */ '2;1');

FILE_NAME(
/* name */ 'Bearing_02.step',
/* time_stamp */ '2026-10-05T21:54:13-07:00',
/* author */ (''),
/* organization */ (''),
/* preprocessor_version */ 'ST-DEVELOPER v20.2',
/* originating_system */ 'Autodesk Translation Framework v15.15.0.0',
/* authorisation */ '');

FILE_SCHEMA (('AUTOMOTIVE_DESIGN { 1 0 10303 214 3 1 1 }'));
ENDSEC;

DATA;
#10=MECHANICAL_DESIGN_GEOMETRIC_PRESENTATION_REPRESENTATION('',(#203,#204,#205,#206,#207,#208,#209,#210,#211,#212),#43781);
#57=SPHERICAL_SURFACE('',#13967,3.56616156686793);
#58=SPHERICAL_SURFACE('',#13969,3.56616156686793);
#59=SPHERICAL_SURFACE('',#13971,3.56616156686793);
#60=SPHERICAL_SURFACE('',#13973,3.56616156686793);
#61=SPHERICAL_SURFACE('',#13975,3.56616156686793);
#62=SPHERICAL_SURFACE('',#13977,3.56616156686793);
#63=SPHERICAL_SURFACE('',#13979,3.56616156686793);
#64=SPHERICAL_SURFACE('',#14033,3.56616156686792);
#65=SPHERICAL_SURFACE('',#14047,3.56616156686792);
#66=SPHERICAL_SURFACE('',#14061,3.56616156686792);
#67=SPHERICAL_SURFACE('',#14075,3.56616156686792);
#68=SPHERICAL_SURFACE('',#14089,3.56616156686792);
#69=SPHERICAL_SURFACE('',#14103,3.56616156686792);
#70=SPHERICAL_SURFACE('',#14113,3.56616156686792);
#103=CONICAL_SURFACE('',#13956,8.14999999999999,0.785398163397436);
#104=CONICAL_SURFACE('',#13959,7.5,0.785398163397437);
#105=CONICAL_SURFACE('',#14015,20.35,0.785398163397442);
#106=CONICAL_SURFACE('',#14018,21.,0.785398163397442);
#130=TOROIDAL_SURFACE('',#13941,14.25,3.56616156686793);
#131=TOROIDAL_SURFACE('',#13945,7.9875,0.4875);
#132=TOROIDAL_SURFACE('',#13951,7.9875,0.4875);
#133=TOROIDAL_SURFACE('',#13981,16.3271153846154,0.0585);
#134=TOROIDAL_SURFACE('',#13986,16.0931153846154,0.0585);
#135=TOROIDAL_SURFACE('',#13990,16.3271153846154,0.0585);
#136=TOROIDAL_SURFACE('',#13994,16.0931153846154,0.0585);
#137=TOROIDAL_SURFACE('',#14006,14.25,3.56616156686793);
#138=TOROIDAL_SURFACE('',#14029,2.5198520116158,1.69469015025);
#139=TOROIDAL_SURFACE('',#14043,2.5198520116158,1.69469015025);
#140=TOROIDAL_SURFACE('',#14057,2.5198520116158,1.69469015025);
#141=TOROIDAL_SURFACE('',#14071,2.5198520116158,1.69469015025);
#142=TOROIDAL_SURFACE('',#14085,2.5198520116158,1.69469015025);
#143=TOROIDAL_SURFACE('',#14099,2.5198520116158,1.69469015025);
#144=TOROIDAL_SURFACE('',#14123,2.5198520116158,1.69469015025);
#178=SHAPE_REPRESENTATION_RELATIONSHIP('SRR','None',#43816,#186);
#186=ADVANCED_BREP_SHAPE_REPRESENTATION('',(#247,#248,#249,#250,#251,#252,
#253,#254,#255,#256),#43776);
#203=STYLED_ITEM('',(#43863),#247);
#204=STYLED_ITEM('',(#43863),#248);
#205=STYLED_ITEM('',(#43863),#249);
#206=STYLED_ITEM('',(#43863),#250);
#207=STYLED_ITEM('',(#43863),#251);
#208=STYLED_ITEM('',(#43863),#252);
#209=STYLED_ITEM('',(#43863),#253);
#210=STYLED_ITEM('',(#43863),#254);
#211=STYLED_ITEM('',(#43863),#255);
#212=STYLED_ITEM('',(#43863),#256);
#247=MANIFOLD_SOLID_BREP('Body1',#13063);
#248=MANIFOLD_SOLID_BREP('Body2',#13064);
#249=MANIFOLD_SOLID_BREP('Body3',#13065);
#250=MANIFOLD_SOLID_BREP('Body4',#13066);
#251=MANIFOLD_SOLID_BREP('Body5',#13067);
#252=MANIFOLD_SOLID_BREP('Body6',#13068);
#253=MANIFOLD_SOLID_BREP('Body7',#13069);
#254=MANIFOLD_SOLID_BREP('Body8',#13070);
#255=MANIFOLD_SOLID_BREP('Body9',#13071);
#256=MANIFOLD_SOLID_BREP('Body10',#13072);
#333=FACE_BOUND('',#2475,.T.);
#334=FACE_BOUND('',#2477,.T.);
#335=FACE_BOUND('',#2500,.T.);
#336=FACE_BOUND('',#2502,.T.);
#337=FACE_BOUND('',#2504,.T.);
#338=FACE_BOUND('',#2506,.T.);
#339=FACE_BOUND('',#2508,.T.);
#340=FACE_BOUND('',#2510,.T.);
#341=FACE_BOUND('',#2512,.T.);
#342=FACE_BOUND('',#2513,.T.);
#343=FACE_BOUND('',#2515,.T.);
#344=FACE_BOUND('',#2516,.T.);
#345=FACE_BOUND('',#2518,.T.);
#346=FACE_BOUND('',#2519,.T.);
#347=FACE_BOUND('',#2521,.T.);
#348=FACE_BOUND('',#2522,.T.);
#349=FACE_BOUND('',#2524,.T.);
#350=FACE_BOUND('',#2525,.T.);
#351=FACE_BOUND('',#2527,.T.);
#352=FACE_BOUND('',#2528,.T.);
#353=FACE_BOUND('',#2530,.T.);
#354=FACE_BOUND('',#2531,.T.);
#355=FACE_BOUND('',#2533,.T.);
#356=FACE_BOUND('',#2534,.T.);
#357=FACE_BOUND('',#2536,.T.);
#358=FACE_BOUND('',#2537,.T.);
#359=FACE_BOUND('',#2539,.T.);
#360=FACE_BOUND('',#2540,.T.);
#361=FACE_BOUND('',#2542,.T.);
#362=FACE_BOUND('',#2543,.T.);
#363=FACE_BOUND('',#2545,.T.);
#364=FACE_BOUND('',#2546,.T.);
#365=FACE_BOUND('',#2548,.T.);
#366=FACE_BOUND('',#2549,.T.);
#367=FACE_BOUND('',#2551,.T.);
#368=FACE_BOUND('',#2552,.T.);
#369=FACE_BOUND('',#2558,.T.);
#370=FACE_BOUND('',#2560,.T.);
#371=FACE_BOUND('',#2566,.T.);
#372=FACE_BOUND('',#2568,.T.);
#373=FACE_BOUND('',#2578,.T.);
#374=FACE_BOUND('',#2580,.T.);
#375=FACE_BOUND('',#2590,.T.);
#376=FACE_BOUND('',#2592,.T.);
#377=FACE_BOUND('',#2602,.T.);
#378=FACE_BOUND('',#2604,.T.);
#379=FACE_BOUND('',#2614,.T.);
#380=FACE_BOUND('',#2616,.T.);
#381=FACE_BOUND('',#2626,.T.);
#382=FACE_BOUND('',#2628,.T.);
#695=B_SPLINE_CURVE_WITH_KNOTS('',3,(#39598,#39599,#39600,#39601,#39602,
#39603),.UNSPECIFIED.,.F.,.F.,(4,2,4),(0.436494357616827,0.49057908163088,
0.523269669927392),.UNSPECIFIED.);
#696=B_SPLINE_CURVE_WITH_KNOTS('',3,(#39605,#39606,#39607,#39608,#39609,
#39610,#39611,#39612,#39613,#39614,#39615,#39616,#39617,#39618,#39619,#39620,
#39621,#39622,#39623),.UNSPECIFIED.,.F.,.F.,(4,3,3,3,3,3,4),(1.21344063784114,
1.25510987200879,1.29073244309217,1.33189452838103,1.37317594357341,1.41463545273866,
1.43283480298246),.UNSPECIFIED.);
#697=B_SPLINE_CURVE_WITH_KNOTS('',3,(#39625,#39626,#39627,#39628,#39629,
#39630),.UNSPECIFIED.,.F.,.F.,(4,2,4),(0.436494357616828,0.49057908163088,
0.523269669927516),.UNSPECIFIED.);
#698=B_SPLINE_CURVE_WITH_KNOTS('',3,(#39631,#39632,#39633,#39634,#39635,
#39636,#39637,#39638,#39639,#39640,#39641,#39642,#39643,#39644,#39645,#39646,
#39647,#39648,#39649),.UNSPECIFIED.,.F.,.F.,(4,3,3,3,3,3,4),(-1.40481265039417,
-1.36522996541144,-1.32585540726346,-1.28679683363995,-1.26015734748852,
-1.21999608757349,-1.1843388203003),.UNSPECIFIED.);
#699=B_SPLINE_CURVE_WITH_KNOTS('',3,(#39652,#39653,#39654,#39655,#39656,
#39657),.UNSPECIFIED.,.F.,.F.,(4,2,4),(1.43904665659616,1.47173724489264,
1.52582196890669),.UNSPECIFIED.);
#700=B_SPLINE_CURVE_WITH_KNOTS('',3,(#39659,#39660,#39661,#39662,#39663,
#39664,#39665,#39666,#39667,#39668,#39669,#39670,#39671,#39672,#39673,#39674,
#39675,#39676,#39677),.UNSPECIFIED.,.F.,.F.,(4,3,3,3,3,3,4),(-0.110253525235352,
-0.070240741437667,-0.0308586443223014,0.,0.0392000421916667,0.0788707706427855,
0.110060546834446),.UNSPECIFIED.);
#701=B_SPLINE_CURVE_WITH_KNOTS('',3,(#39679,#39680,#39681,#39682,#39683,
#39684),.UNSPECIFIED.,.F.,.F.,(4,2,4),(1.43904665659616,1.47173724489264,
1.52582196890582),.UNSPECIFIED.);
#702=B_SPLINE_CURVE_WITH_KNOTS('',3,(#39685,#39686,#39687,#39688,#39689,
#39690,#39691,#39692,#39693,#39694,#39695,#39696,#39697,#39698,#39699,#39700,
#39701,#39702,#39703),.UNSPECIFIED.,.F.,.F.,(4,3,3,3,3,3,4),(2.53632937909178,
2.57775416224765,2.61898206719527,2.6459019021663,2.68717408326041,2.72876559667488,
2.75562831582286),.UNSPECIFIED.);
#703=B_SPLINE_CURVE_WITH_KNOTS('',3,(#39713,#39714,#39715,#39716,#39717,
#39718,#39719),.UNSPECIFIED.,.F.,.F.,(4,3,4),(1.98904556960248,2.09488046175532,
2.20071535390815),.UNSPECIFIED.);
#704=B_SPLINE_CURVE_WITH_KNOTS('',3,(#39723,#39724,#39725,#39726,#39727,
#39728,#39729),.UNSPECIFIED.,.F.,.F.,(4,3,4),(-0.105611957753097,0.,0.105611957753097),
 .UNSPECIFIED.);
#705=B_SPLINE_CURVE_WITH_KNOTS('',3,(#39734,#39735,#39736,#39737,#39738,
#39739),.UNSPECIFIED.,.F.,.F.,(4,2,4),(-1.17106027221854,-1.06544831446544,
-0.959836356712345),.UNSPECIFIED.);
#706=B_SPLINE_CURVE_WITH_KNOTS('',3,(#39742,#39743,#39744,#39745,#39746,
#39747),.UNSPECIFIED.,.F.,.F.,(4,2,4),(0.941605338724826,1.04744023087766,
1.15327512303049),.UNSPECIFIED.);
#707=B_SPLINE_CURVE_WITH_KNOTS('',3,(#39760,#39761,#39762,#39763,#39764,
#39765),.UNSPECIFIED.,.F.,.F.,(4,2,4),(0.436494357616816,0.49057908163088,
0.523269669927352),.UNSPECIFIED.);
#708=B_SPLINE_CURVE_WITH_KNOTS('',3,(#39767,#39768,#39769,#39770,#39771,
#39772,#39773,#39774,#39775,#39776,#39777,#39778,#39779,#39780,#39781,#39782,
#39783,#39784,#39785),.UNSPECIFIED.,.F.,.F.,(4,3,3,3,3,3,4),(1.21344063784117,
1.2551098720088,1.29073244309219,1.33189452838105,1.37317594357344,1.41463545273871,
1.43283480298249),.UNSPECIFIED.);
#709=B_SPLINE_CURVE_WITH_KNOTS('',3,(#39787,#39788,#39789,#39790,#39791,
#39792),.UNSPECIFIED.,.F.,.F.,(4,2,4),(0.436484426249651,0.490578640084517,
0.523250481795878),.UNSPECIFIED.);
#710=B_SPLINE_CURVE_WITH_KNOTS('',3,(#39793,#39794,#39795,#39796,#39797,
#39798,#39799,#39800,#39801,#39802,#39803,#39804,#39805,#39806,#39807,#39808,
#39809,#39810,#39811),.UNSPECIFIED.,.F.,.F.,(4,3,3,3,3,3,4),(-1.40481265039413,
-1.36522996541145,-1.32585540726349,-1.28679683363998,-1.2601573474885,
-1.21999608757352,-1.18433882030031),.UNSPECIFIED.);
#711=B_SPLINE_CURVE_WITH_KNOTS('',3,(#39814,#39815,#39816,#39817,#39818,
#39819),.UNSPECIFIED.,.F.,.F.,(4,2,4),(1.43906407854219,1.47173592025355,
1.52583013408841),.UNSPECIFIED.);
#712=B_SPLINE_CURVE_WITH_KNOTS('',3,(#39821,#39822,#39823,#39824,#39825,
#39826,#39827,#39828,#39829,#39830,#39831,#39832,#39833,#39834,#39835,#39836,
#39837,#39838,#39839),.UNSPECIFIED.,.F.,.F.,(4,3,3,3,3,3,4),(-0.110253525235351,
-0.0702407414376934,-0.0308586443223274,0.,0.0392000421916682,0.0788707706427895,
0.110060546834446),.UNSPECIFIED.);
#713=B_SPLINE_CURVE_WITH_KNOTS('',3,(#39841,#39842,#39843,#39844,#39845,
#39846),.UNSPECIFIED.,.F.,.F.,(4,2,4),(1.43906407854219,1.47173592025355,
1.52583013408754),.UNSPECIFIED.);
#714=B_SPLINE_CURVE_WITH_KNOTS('',3,(#39847,#39848,#39849,#39850,#39851,
#39852,#39853,#39854,#39855,#39856,#39857,#39858,#39859,#39860,#39861,#39862,
#39863,#39864,#39865),.UNSPECIFIED.,.F.,.F.,(4,3,3,3,3,3,4),(2.53632937909181,
2.57775416224765,2.61898206719527,2.64590190216633,2.68717408326044,2.72876559667489,
2.75562831582288),.UNSPECIFIED.);
#715=B_SPLINE_CURVE_WITH_KNOTS('',3,(#39875,#39876,#39877,#39878,#39879,
#39880,#39881),.UNSPECIFIED.,.F.,.F.,(4,3,4),(1.98904556960249,2.09488046175532,
2.20071535390816),.UNSPECIFIED.);
#716=B_SPLINE_CURVE_WITH_KNOTS('',3,(#39885,#39886,#39887,#39888,#39889,
#39890,#39891),.UNSPECIFIED.,.F.,.F.,(4,3,4),(-0.105611957753097,0.,0.105611957753097),
 .UNSPECIFIED.);
#717=B_SPLINE_CURVE_WITH_KNOTS('',3,(#39896,#39897,#39898,#39899,#39900,
#39901),.UNSPECIFIED.,.F.,.F.,(4,2,4),(-1.17106027221854,-1.06544831446544,
-0.959836356712344),.UNSPECIFIED.);
#718=B_SPLINE_CURVE_WITH_KNOTS('',3,(#39904,#39905,#39906,#39907,#39908,
#39909),.UNSPECIFIED.,.F.,.F.,(4,2,4),(0.941605338724829,1.04744023087766,
1.15327512303049),.UNSPECIFIED.);
#719=B_SPLINE_CURVE_WITH_KNOTS('',3,(#39922,#39923,#39924,#39925,#39926,
#39927),.UNSPECIFIED.,.F.,.F.,(4,2,4),(0.436484426249655,0.490578640084517,
0.523250481795882),.UNSPECIFIED.);
#720=B_SPLINE_CURVE_WITH_KNOTS('',3,(#39929,#39930,#39931,#39932,#39933,
#39934,#39935,#39936,#39937,#39938,#39939,#39940,#39941,#39942,#39943,#39944,
#39945,#39946,#39947),.UNSPECIFIED.,.F.,.F.,(4,3,3,3,3,3,4),(2.53632937909178,
2.57775416224762,2.61898206719525,2.64590190216632,2.68717408326042,2.72876559667488,
2.75562831582289),.UNSPECIFIED.);
#721=B_SPLINE_CURVE_WITH_KNOTS('',3,(#39949,#39950,#39951,#39952,#39953,
#39954),.UNSPECIFIED.,.F.,.F.,(4,2,4),(0.436494357616821,0.49057908163088,
0.523269669927365),.UNSPECIFIED.);
#722=B_SPLINE_CURVE_WITH_KNOTS('',3,(#39955,#39956,#39957,#39958,#39959,
#39960,#39961,#39962,#39963,#39964,#39965,#39966,#39967,#39968,#39969,#39970,
#39971,#39972,#39973),.UNSPECIFIED.,.F.,.F.,(4,3,3,3,3,3,4),(-0.110253525235353,
-0.0702407414376493,-0.0308586443222864,0.,0.0392000421916586,0.0788707706427754,
0.110060546834447),.UNSPECIFIED.);
#723=B_SPLINE_CURVE_WITH_KNOTS('',3,(#39976,#39977,#39978,#39979,#39980,
#39981),.UNSPECIFIED.,.F.,.F.,(4,2,4),(1.43906407854219,1.47173592025355,
1.52583013408841),.UNSPECIFIED.);
#724=B_SPLINE_CURVE_WITH_KNOTS('',3,(#39983,#39984,#39985,#39986,#39987,
#39988,#39989,#39990,#39991,#39992,#39993,#39994,#39995,#39996,#39997,#39998,
#39999,#40000,#40001),.UNSPECIFIED.,.F.,.F.,(4,3,3,3,3,3,4),(-1.40481265039415,
-1.36522996541142,-1.32585540726345,-1.28679683363994,-1.26015734748852,
-1.21999608757345,-1.18433882030032),.UNSPECIFIED.);
#725=B_SPLINE_CURVE_WITH_KNOTS('',3,(#40003,#40004,#40005,#40006,#40007,
#40008),.UNSPECIFIED.,.F.,.F.,(4,2,4),(1.43906407854219,1.47173592025355,
1.52583013408753),.UNSPECIFIED.);
#726=B_SPLINE_CURVE_WITH_KNOTS('',3,(#40009,#40010,#40011,#40012,#40013,
#40014,#40015,#40016,#40017,#40018,#40019,#40020,#40021,#40022,#40023,#40024,
#40025,#40026,#40027),.UNSPECIFIED.,.F.,.F.,(4,3,3,3,3,3,4),(1.21344063784118,
1.25510987200885,1.29073244309219,1.33189452838105,1.37317594357345,1.41463545273868,
1.43283480298247),.UNSPECIFIED.);
#727=B_SPLINE_CURVE_WITH_KNOTS('',3,(#40037,#40038,#40039,#40040,#40041,
#40042,#40043),.UNSPECIFIED.,.F.,.F.,(4,3,4),(1.98904556960249,2.09488046175532,
2.20071535390815),.UNSPECIFIED.);
#728=B_SPLINE_CURVE_WITH_KNOTS('',3,(#40047,#40048,#40049,#40050,#40051,
#40052,#40053),.UNSPECIFIED.,.F.,.F.,(4,3,4),(-0.105611957753096,0.,0.105611957753097),
 .UNSPECIFIED.);
#729=B_SPLINE_CURVE_WITH_KNOTS('',3,(#40058,#40059,#40060,#40061,#40062,
#40063),.UNSPECIFIED.,.F.,.F.,(4,2,4),(-1.17106027221854,-1.06544831446544,
-0.959836356712344),.UNSPECIFIED.);
#730=B_SPLINE_CURVE_WITH_KNOTS('',3,(#40066,#40067,#40068,#40069,#40070,
#40071),.UNSPECIFIED.,.F.,.F.,(4,2,4),(0.941605338724827,1.04744023087766,
1.15327512303049),.UNSPECIFIED.);
#731=B_SPLINE_CURVE_WITH_KNOTS('',3,(#40084,#40085,#40086,#40087,#40088,
#40089),.UNSPECIFIED.,.F.,.F.,(4,2,4),(0.436494357616822,0.49057908163088,
0.523269669927398),.UNSPECIFIED.);
#732=B_SPLINE_CURVE_WITH_KNOTS('',3,(#40091,#40092,#40093,#40094,#40095,
#40096,#40097,#40098,#40099,#40100,#40101,#40102,#40103,#40104,#40105,#40106,
#40107,#40108,#40109),.UNSPECIFIED.,.F.,.F.,(4,3,3,3,3,3,4),(2.53632937909185,
2.57775416224773,2.61898206719535,2.64590190216638,2.6871740832605,2.72876559667492,
2.75562831582295),.UNSPECIFIED.);
#733=B_SPLINE_CURVE_WITH_KNOTS('',3,(#40111,#40112,#40113,#40114,#40115,
#40116),.UNSPECIFIED.,.F.,.F.,(4,2,4),(0.436484426249657,0.490578640084517,
0.523250481796065),.UNSPECIFIED.);
#734=B_SPLINE_CURVE_WITH_KNOTS('',3,(#40117,#40118,#40119,#40120,#40121,
#40122,#40123,#40124,#40125,#40126,#40127,#40128,#40129,#40130,#40131,#40132,
#40133,#40134,#40135),.UNSPECIFIED.,.F.,.F.,(4,3,3,3,3,3,4),(-0.110253525235377,
-0.070240741437708,-0.0308586443223363,0.,0.03920004219167,0.0788707706428437,
0.110060546834472),.UNSPECIFIED.);
#735=B_SPLINE_CURVE_WITH_KNOTS('',3,(#40138,#40139,#40140,#40141,#40142,
#40143),.UNSPECIFIED.,.F.,.F.,(4,2,4),(1.43904665659616,1.47173724489264,
1.52582196890669),.UNSPECIFIED.);
#736=B_SPLINE_CURVE_WITH_KNOTS('',3,(#40145,#40146,#40147,#40148,#40149,
#40150,#40151,#40152,#40153,#40154,#40155,#40156,#40157,#40158,#40159,#40160,
#40161,#40162,#40163),.UNSPECIFIED.,.F.,.F.,(4,3,3,3,3,3,4),(-1.40481265039411,
-1.36522996541141,-1.32585540726345,-1.28679683363994,-1.26015734748849,
-1.21999608757351,-1.1843388203003),.UNSPECIFIED.);
#737=B_SPLINE_CURVE_WITH_KNOTS('',3,(#40165,#40166,#40167,#40168,#40169,
#40170),.UNSPECIFIED.,.F.,.F.,(4,2,4),(1.43904665659616,1.47173724489264,
1.52582196890583),.UNSPECIFIED.);
#738=B_SPLINE_CURVE_WITH_KNOTS('',3,(#40171,#40172,#40173,#40174,#40175,
#40176,#40177,#40178,#40179,#40180,#40181,#40182,#40183,#40184,#40185,#40186,
#40187,#40188,#40189),.UNSPECIFIED.,.F.,.F.,(4,3,3,3,3,3,4),(1.2134406378412,
1.25510987200883,1.29073244309221,1.33189452838107,1.37317594357346,1.41463545273868,
1.43283480298249),.UNSPECIFIED.);
#739=B_SPLINE_CURVE_WITH_KNOTS('',3,(#40199,#40200,#40201,#40202,#40203,
#40204,#40205),.UNSPECIFIED.,.F.,.F.,(4,3,4),(1.98904556960248,2.09488046175532,
2.20071535390815),.UNSPECIFIED.);
#740=B_SPLINE_CURVE_WITH_KNOTS('',3,(#40209,#40210,#40211,#40212,#40213,
#40214,#40215),.UNSPECIFIED.,.F.,.F.,(4,3,4),(-0.105611957753097,0.,0.105611957753097),
 .UNSPECIFIED.);
#741=B_SPLINE_CURVE_WITH_KNOTS('',3,(#40220,#40221,#40222,#40223,#40224,
#40225),.UNSPECIFIED.,.F.,.F.,(4,2,4),(-1.17106027221854,-1.06544831446544,
-0.959836356712344),.UNSPECIFIED.);
#742=B_SPLINE_CURVE_WITH_KNOTS('',3,(#40228,#40229,#40230,#40231,#40232,
#40233),.UNSPECIFIED.,.F.,.F.,(4,2,4),(0.941605338724826,1.04744023087766,
1.15327512303049),.UNSPECIFIED.);
#743=B_SPLINE_CURVE_WITH_KNOTS('',3,(#40246,#40247,#40248,#40249,#40250,
#40251),.UNSPECIFIED.,.F.,.F.,(4,2,4),(0.436494357616821,0.49057908163088,
0.523269669927355),.UNSPECIFIED.);
#744=B_SPLINE_CURVE_WITH_KNOTS('',3,(#40253,#40254,#40255,#40256,#40257,
#40258,#40259,#40260,#40261,#40262,#40263,#40264,#40265,#40266,#40267,#40268,
#40269,#40270,#40271),.UNSPECIFIED.,.F.,.F.,(4,3,3,3,3,3,4),(2.53632937909179,
2.57775416224772,2.61898206719534,2.64590190216632,2.68717408326042,2.72876559667486,
2.75562831582289),.UNSPECIFIED.);
#745=B_SPLINE_CURVE_WITH_KNOTS('',3,(#40273,#40274,#40275,#40276,#40277,
#40278),.UNSPECIFIED.,.F.,.F.,(4,2,4),(0.436494357616821,0.49057908163088,
0.523269669927355),.UNSPECIFIED.);
#746=B_SPLINE_CURVE_WITH_KNOTS('',3,(#40279,#40280,#40281,#40282,#40283,
#40284,#40285,#40286,#40287,#40288,#40289,#40290,#40291,#40292,#40293,#40294,
#40295,#40296,#40297),.UNSPECIFIED.,.F.,.F.,(4,3,3,3,3,3,4),(-0.110253525235352,
-0.0702407414377446,-0.0308586443223844,0.,0.039200042191676,0.0788707706427867,
0.110060546834448),.UNSPECIFIED.);
#747=B_SPLINE_CURVE_WITH_KNOTS('',3,(#40300,#40301,#40302,#40303,#40304,
#40305),.UNSPECIFIED.,.F.,.F.,(4,2,4),(1.43904665659616,1.47173724489264,
1.5258219689067),.UNSPECIFIED.);
#748=B_SPLINE_CURVE_WITH_KNOTS('',3,(#40307,#40308,#40309,#40310,#40311,
#40312,#40313,#40314,#40315,#40316,#40317,#40318,#40319,#40320,#40321,#40322,
#40323,#40324,#40325),.UNSPECIFIED.,.F.,.F.,(4,3,3,3,3,3,4),(-1.40481265039416,
-1.36522996541145,-1.32585540726348,-1.28679683363997,-1.26015734748853,
-1.21999608757355,-1.18433882030033),.UNSPECIFIED.);
#749=B_SPLINE_CURVE_WITH_KNOTS('',3,(#40327,#40328,#40329,#40330,#40331,
#40332),.UNSPECIFIED.,.F.,.F.,(4,2,4),(1.43904665659616,1.47173724489264,
1.52582196890582),.UNSPECIFIED.);
#750=B_SPLINE_CURVE_WITH_KNOTS('',3,(#40333,#40334,#40335,#40336,#40337,
#40338,#40339,#40340,#40341,#40342,#40343,#40344,#40345,#40346,#40347,#40348,
#40349,#40350,#40351),.UNSPECIFIED.,.F.,.F.,(4,3,3,3,3,3,4),(1.21344063784118,
1.25510987200879,1.29073244309219,1.33189452838105,1.37317594357344,1.41463545273868,
1.43283480298247),.UNSPECIFIED.);
#751=B_SPLINE_CURVE_WITH_KNOTS('',3,(#40361,#40362,#40363,#40364,#40365,
#40366,#40367),.UNSPECIFIED.,.F.,.F.,(4,3,4),(1.98904556960248,2.09488046175532,
2.20071535390815),.UNSPECIFIED.);
#752=B_SPLINE_CURVE_WITH_KNOTS('',3,(#40371,#40372,#40373,#40374,#40375,
#40376,#40377),.UNSPECIFIED.,.F.,.F.,(4,3,4),(-0.105611957753098,0.,0.105611957753098),
 .UNSPECIFIED.);
#753=B_SPLINE_CURVE_WITH_KNOTS('',3,(#40382,#40383,#40384,#40385,#40386,
#40387),.UNSPECIFIED.,.F.,.F.,(4,2,4),(-1.17106027221854,-1.06544831446544,
-0.959836356712345),.UNSPECIFIED.);
#754=B_SPLINE_CURVE_WITH_KNOTS('',3,(#40390,#40391,#40392,#40393,#40394,
#40395),.UNSPECIFIED.,.F.,.F.,(4,2,4),(0.941605338724826,1.04744023087766,
1.15327512303049),.UNSPECIFIED.);
#755=B_SPLINE_CURVE_WITH_KNOTS('',3,(#40408,#40409,#40410,#40411,#40412,
#40413,#40414,#40415,#40416,#40417,#40418,#40419,#40420,#40421,#40422,#40423,
#40424,#40425,#40426),.UNSPECIFIED.,.F.,.F.,(4,3,3,3,3,3,4),(2.47883976068978,
2.51859129056809,2.55786629068885,2.58890030752247,2.62818560996811,2.66809093310445,
2.69915383275782),.UNSPECIFIED.);
#756=B_SPLINE_CURVE_WITH_KNOTS('',3,(#40428,#40429,#40430,#40431,#40432,
#40433),.UNSPECIFIED.,.F.,.F.,(4,2,4),(-0.523250481795672,-0.490578640084517,
-0.436484426249653),.UNSPECIFIED.);
#757=B_SPLINE_CURVE_WITH_KNOTS('',3,(#40435,#40436,#40437,#40438,#40439,
#40440,#40441,#40442,#40443,#40444,#40445,#40446,#40447,#40448,#40449,#40450,
#40451,#40452,#40453),.UNSPECIFIED.,.F.,.F.,(4,3,3,3,3,3,4),(-0.109726413656553,
-0.0680893754924848,-0.0267736956128723,0.,0.0412006233150074,0.082597721206199,
0.109572523074534),.UNSPECIFIED.);
#758=B_SPLINE_CURVE_WITH_KNOTS('',3,(#40454,#40455,#40456,#40457,#40458,
#40459),.UNSPECIFIED.,.F.,.F.,(4,2,4),(-0.523250481795879,-0.490578640084517,
-0.43648442624966),.UNSPECIFIED.);
#759=B_SPLINE_CURVE_WITH_KNOTS('',3,(#40462,#40463,#40464,#40465,#40466,
#40467),.UNSPECIFIED.,.F.,.F.,(4,2,4),(1.43904665659616,1.47173724489264,
1.5258219689067),.UNSPECIFIED.);
#760=B_SPLINE_CURVE_WITH_KNOTS('',3,(#40469,#40470,#40471,#40472,#40473,
#40474,#40475,#40476,#40477,#40478,#40479,#40480,#40481,#40482,#40483,#40484,
#40485,#40486,#40487),.UNSPECIFIED.,.F.,.F.,(4,3,3,3,3,3,4),(-1.40481265039414,
-1.36522996541144,-1.32585540726348,-1.28679683363997,-1.26015734748851,
-1.21999608757358,-1.18433882030032),.UNSPECIFIED.);
#761=B_SPLINE_CURVE_WITH_KNOTS('',3,(#40489,#40490,#40491,#40492,#40493,
#40494),.UNSPECIFIED.,.F.,.F.,(4,2,4),(1.43904665659617,1.47173724489264,
1.52582196890583),.UNSPECIFIED.);
#762=B_SPLINE_CURVE_WITH_KNOTS('',3,(#40495,#40496,#40497,#40498,#40499,
#40500,#40501,#40502,#40503,#40504,#40505,#40506,#40507,#40508,#40509,#40510,
#40511,#40512,#40513),.UNSPECIFIED.,.F.,.F.,(4,3,3,3,3,3,4),(1.21344063784118,
1.25510987200878,1.29073244309219,1.33189452838105,1.37317594357344,1.41463545273868,
1.43283480298247),.UNSPECIFIED.);
#763=B_SPLINE_CURVE_WITH_KNOTS('',3,(#40519,#40520,#40521,#40522,#40523,
#40524),.UNSPECIFIED.,.F.,.F.,(4,2,4),(0.959836356712344,1.06544831446544,
1.17106027221854),.UNSPECIFIED.);
#764=B_SPLINE_CURVE_WITH_KNOTS('',3,(#40528,#40529,#40530,#40531,#40532,
#40533),.UNSPECIFIED.,.F.,.F.,(4,2,4),(-1.15327512303049,-1.04744023087766,
-0.941605338724826),.UNSPECIFIED.);
#765=B_SPLINE_CURVE_WITH_KNOTS('',3,(#40540,#40541,#40542,#40543,#40544,
#40545,#40546),.UNSPECIFIED.,.F.,.F.,(4,3,4),(1.98904556960249,2.09488046175532,
2.20071535390815),.UNSPECIFIED.);
#766=B_SPLINE_CURVE_WITH_KNOTS('',3,(#40550,#40551,#40552,#40553,#40554,
#40555,#40556),.UNSPECIFIED.,.F.,.F.,(4,3,4),(-0.105611957753097,0.,0.105611957753097),
 .UNSPECIFIED.);
#767=B_SPLINE_CURVE_WITH_KNOTS('',3,(#40571,#40572,#40573,#40574,#40575,
#40576,#40577),.UNSPECIFIED.,.F.,.F.,(4,3,4),(1.98904556960249,2.09488046175532,
2.20071535390815),.UNSPECIFIED.);
#768=B_SPLINE_CURVE_WITH_KNOTS('',3,(#40581,#40582,#40583,#40584,#40585,
#40586,#40587),.UNSPECIFIED.,.F.,.F.,(4,3,4),(-0.105611957753096,0.,0.105611957753097),
 .UNSPECIFIED.);
#769=B_SPLINE_CURVE_WITH_KNOTS('',3,(#40592,#40593,#40594,#40595,#40596,
#40597),.UNSPECIFIED.,.F.,.F.,(4,2,4),(-1.17106027221854,-1.06544831446544,
-0.959836356712344),.UNSPECIFIED.);
#770=B_SPLINE_CURVE_WITH_KNOTS('',3,(#40600,#40601,#40602,#40603,#40604,
#40605),.UNSPECIFIED.,.F.,.F.,(4,2,4),(0.941605338724827,1.04744023087766,
1.15327512303049),.UNSPECIFIED.);
#771=B_SPLINE_CURVE_WITH_KNOTS('',3,(#40618,#40619,#40620,#40621,#40622,
#40623),.UNSPECIFIED.,.F.,.F.,(4,2,4),(0.43648442624966,0.490578640084517,
0.523250481795913),.UNSPECIFIED.);
#772=B_SPLINE_CURVE_WITH_KNOTS('',3,(#40625,#40626,#40627,#40628,#40629,
#40630,#40631,#40632,#40633,#40634,#40635,#40636,#40637,#40638,#40639,#40640,
#40641,#40642,#40643),.UNSPECIFIED.,.F.,.F.,(4,3,3,3,3,3,4),(1.21344063784115,
1.25510987200874,1.29073244309218,1.33189452838104,1.37317594357343,1.41463545273866,
1.43283480298248),.UNSPECIFIED.);
#773=B_SPLINE_CURVE_WITH_KNOTS('',3,(#40645,#40646,#40647,#40648,#40649,
#40650),.UNSPECIFIED.,.F.,.F.,(4,2,4),(0.436494357616825,0.49057908163088,
0.523269669927497),.UNSPECIFIED.);
#774=B_SPLINE_CURVE_WITH_KNOTS('',3,(#40651,#40652,#40653,#40654,#40655,
#40656,#40657,#40658,#40659,#40660,#40661,#40662,#40663,#40664,#40665,#40666,
#40667,#40668,#40669),.UNSPECIFIED.,.F.,.F.,(4,3,3,3,3,3,4),(-1.40481265039423,
-1.36522996541152,-1.32585540726357,-1.28679683364005,-1.26015734748857,
-1.2199960875736,-1.18433882030035),.UNSPECIFIED.);
#775=B_SPLINE_CURVE_WITH_KNOTS('',3,(#40672,#40673,#40674,#40675,#40676,
#40677),.UNSPECIFIED.,.F.,.F.,(4,2,4),(1.43906407854219,1.47173592025355,
1.52583013408841),.UNSPECIFIED.);
#776=B_SPLINE_CURVE_WITH_KNOTS('',3,(#40679,#40680,#40681,#40682,#40683,
#40684,#40685,#40686,#40687,#40688,#40689,#40690,#40691,#40692,#40693,#40694,
#40695,#40696,#40697),.UNSPECIFIED.,.F.,.F.,(4,3,3,3,3,3,4),(-0.110253525235352,
-0.0702407414376601,-0.030858644322292,0.,0.0392000421916706,0.0788707706427867,
0.110060546834447),.UNSPECIFIED.);
#777=B_SPLINE_CURVE_WITH_KNOTS('',3,(#40699,#40700,#40701,#40702,#40703,
#40704),.UNSPECIFIED.,.F.,.F.,(4,2,4),(1.43906407854219,1.47173592025355,
1.52583013408754),.UNSPECIFIED.);
#778=B_SPLINE_CURVE_WITH_KNOTS('',3,(#40705,#40706,#40707,#40708,#40709,
#40710,#40711,#40712,#40713,#40714,#40715,#40716,#40717,#40718,#40719,#40720,
#40721,#40722,#40723),.UNSPECIFIED.,.F.,.F.,(4,3,3,3,3,3,4),(2.53632937909179,
2.57775416224768,2.61898206719531,2.64590190216631,2.68717408326042,2.72876559667485,
2.75562831582286),.UNSPECIFIED.);
#1125=PLANE('',#13965);
#1126=PLANE('',#13966);
#1127=PLANE('',#14023);
#1128=PLANE('',#14024);
#1129=PLANE('',#14025);
#1130=PLANE('',#14026);
#1131=PLANE('',#14027);
#1132=PLANE('',#14028);
#1133=PLANE('',#14133);
#1134=PLANE('',#14134);
#1135=PLANE('',#14135);
#1136=PLANE('',#14136);
#1137=PLANE('',#14137);
#1138=PLANE('',#14140);
#1139=PLANE('',#14145);
#1140=PLANE('',#14146);
#1141=PLANE('',#14147);
#1142=PLANE('',#14150);
#1143=PLANE('',#14161);
#1144=PLANE('',#14162);
#1145=PLANE('',#14163);
#1146=PLANE('',#14164);
#1147=PLANE('',#14165);
#1148=PLANE('',#14168);
#1149=PLANE('',#14179);
#1150=PLANE('',#14180);
#1151=PLANE('',#14181);
#1152=PLANE('',#14182);
#1153=PLANE('',#14183);
#1154=PLANE('',#14186);
#1155=PLANE('',#14197);
#1156=PLANE('',#14198);
#1157=PLANE('',#14199);
#1158=PLANE('',#14200);
#1159=PLANE('',#14201);
#1160=PLANE('',#14204);
#1161=PLANE('',#14215);
#1162=PLANE('',#14216);
#1163=PLANE('',#14217);
#1164=PLANE('',#14218);
#1165=PLANE('',#14219);
#1166=PLANE('',#14222);
#1167=PLANE('',#14233);
#1168=PLANE('',#14234);
#1169=PLANE('',#14235);
#1170=PLANE('',#14236);
#1171=PLANE('',#14237);
#1172=PLANE('',#14240);
#1173=PLANE('',#14245);
#1174=PLANE('',#14248);
#1660=FACE_OUTER_BOUND('',#2466,.T.);
#1661=FACE_OUTER_BOUND('',#2467,.T.);
#1662=FACE_OUTER_BOUND('',#2468,.T.);
#1663=FACE_OUTER_BOUND('',#2469,.T.);
#1664=FACE_OUTER_BOUND('',#2470,.T.);
#1665=FACE_OUTER_BOUND('',#2471,.T.);
#1666=FACE_OUTER_BOUND('',#2472,.T.);
#1667=FACE_OUTER_BOUND('',#2473,.T.);
#1668=FACE_OUTER_BOUND('',#2474,.T.);
#1669=FACE_OUTER_BOUND('',#2476,.T.);
#1670=FACE_OUTER_BOUND('',#2478,.T.);
#1671=FACE_OUTER_BOUND('',#2479,.T.);
#1672=FACE_OUTER_BOUND('',#2480,.T.);
#1673=FACE_OUTER_BOUND('',#2481,.T.);
#1674=FACE_OUTER_BOUND('',#2482,.T.);
#1675=FACE_OUTER_BOUND('',#2483,.T.);
#1676=FACE_OUTER_BOUND('',#2484,.T.);
#1677=FACE_OUTER_BOUND('',#2485,.T.);
#1678=FACE_OUTER_BOUND('',#2486,.T.);
#1679=FACE_OUTER_BOUND('',#2487,.T.);
#1680=FACE_OUTER_BOUND('',#2488,.T.);
#1681=FACE_OUTER_BOUND('',#2489,.T.);
#1682=FACE_OUTER_BOUND('',#2490,.T.);
#1683=FACE_OUTER_BOUND('',#2491,.T.);
#1684=FACE_OUTER_BOUND('',#2492,.T.);
#1685=FACE_OUTER_BOUND('',#2493,.T.);
#1686=FACE_OUTER_BOUND('',#2494,.T.);
#1687=FACE_OUTER_BOUND('',#2495,.T.);
#1688=FACE_OUTER_BOUND('',#2496,.T.);
#1689=FACE_OUTER_BOUND('',#2497,.T.);
#1690=FACE_OUTER_BOUND('',#2498,.T.);
#1691=FACE_OUTER_BOUND('',#2499,.T.);
#1692=FACE_OUTER_BOUND('',#2501,.T.);
#1693=FACE_OUTER_BOUND('',#2503,.T.);
#1694=FACE_OUTER_BOUND('',#2505,.T.);
#1695=FACE_OUTER_BOUND('',#2507,.T.);
#1696=FACE_OUTER_BOUND('',#2509,.T.);
#1697=FACE_OUTER_BOUND('',#2511,.T.);
#1698=FACE_OUTER_BOUND('',#2514,.T.);
#1699=FACE_OUTER_BOUND('',#2517,.T.);
#1700=FACE_OUTER_BOUND('',#2520,.T.);
#1701=FACE_OUTER_BOUND('',#2523,.T.);
#1702=FACE_OUTER_BOUND('',#2526,.T.);
#1703=FACE_OUTER_BOUND('',#2529,.T.);
#1704=FACE_OUTER_BOUND('',#2532,.T.);
#1705=FACE_OUTER_BOUND('',#2535,.T.);
#1706=FACE_OUTER_BOUND('',#2538,.T.);
#1707=FACE_OUTER_BOUND('',#2541,.T.);
#1708=FACE_OUTER_BOUND('',#2544,.T.);
#1709=FACE_OUTER_BOUND('',#2547,.T.);
#1710=FACE_OUTER_BOUND('',#2550,.T.);
#1711=FACE_OUTER_BOUND('',#2553,.T.);
#1712=FACE_OUTER_BOUND('',#2554,.T.);
#1713=FACE_OUTER_BOUND('',#2555,.T.);
#1714=FACE_OUTER_BOUND('',#2556,.T.);
#1715=FACE_OUTER_BOUND('',#2557,.T.);
#1716=FACE_OUTER_BOUND('',#2559,.T.);
#1717=FACE_OUTER_BOUND('',#2561,.T.);
#1718=FACE_OUTER_BOUND('',#2562,.T.);
#1719=FACE_OUTER_BOUND('',#2563,.T.);
#1720=FACE_OUTER_BOUND('',#2564,.T.);
#1721=FACE_OUTER_BOUND('',#2565,.T.);
#1722=FACE_OUTER_BOUND('',#2567,.T.);
#1723=FACE_OUTER_BOUND('',#2569,.T.);
#1724=FACE_OUTER_BOUND('',#2570,.T.);
#1725=FACE_OUTER_BOUND('',#2571,.T.);
#1726=FACE_OUTER_BOUND('',#2572,.T.);
#1727=FACE_OUTER_BOUND('',#2573,.T.);
#1728=FACE_OUTER_BOUND('',#2574,.T.);
#1729=FACE_OUTER_BOUND('',#2575,.T.);
#1730=FACE_OUTER_BOUND('',#2576,.T.);
#1731=FACE_OUTER_BOUND('',#2577,.T.);
#1732=FACE_OUTER_BOUND('',#2579,.T.);
#1733=FACE_OUTER_BOUND('',#2581,.T.);
#1734=FACE_OUTER_BOUND('',#2582,.T.);
#1735=FACE_OUTER_BOUND('',#2583,.T.);
#1736=FACE_OUTER_BOUND('',#2584,.T.);
#1737=FACE_OUTER_BOUND('',#2585,.T.);
#1738=FACE_OUTER_BOUND('',#2586,.T.);
#1739=FACE_OUTER_BOUND('',#2587,.T.);
#1740=FACE_OUTER_BOUND('',#2588,.T.);
#1741=FACE_OUTER_BOUND('',#2589,.T.);
#1742=FACE_OUTER_BOUND('',#2591,.T.);
#1743=FACE_OUTER_BOUND('',#2593,.T.);
#1744=FACE_OUTER_BOUND('',#2594,.T.);
#1745=FACE_OUTER_BOUND('',#2595,.T.);
#1746=FACE_OUTER_BOUND('',#2596,.T.);
#1747=FACE_OUTER_BOUND('',#2597,.T.);
#1748=FACE_OUTER_BOUND('',#2598,.T.);
#1749=FACE_OUTER_BOUND('',#2599,.T.);
#1750=FACE_OUTER_BOUND('',#2600,.T.);
#1751=FACE_OUTER_BOUND('',#2601,.T.);
#1752=FACE_OUTER_BOUND('',#2603,.T.);
#1753=FACE_OUTER_BOUND('',#2605,.T.);
#1754=FACE_OUTER_BOUND('',#2606,.T.);
#1755=FACE_OUTER_BOUND('',#2607,.T.);
#1756=FACE_OUTER_BOUND('',#2608,.T.);
#1757=FACE_OUTER_BOUND('',#2609,.T.);
#1758=FACE_OUTER_BOUND('',#2610,.T.);
#1759=FACE_OUTER_BOUND('',#2611,.T.);
#1760=FACE_OUTER_BOUND('',#2612,.T.);
#1761=FACE_OUTER_BOUND('',#2613,.T.);
#1762=FACE_OUTER_BOUND('',#2615,.T.);
#1763=FACE_OUTER_BOUND('',#2617,.T.);
#1764=FACE_OUTER_BOUND('',#2618,.T.);
#1765=FACE_OUTER_BOUND('',#2619,.T.);
#1766=FACE_OUTER_BOUND('',#2620,.T.);
#1767=FACE_OUTER_BOUND('',#2621,.T.);
#1768=FACE_OUTER_BOUND('',#2622,.T.);
#1769=FACE_OUTER_BOUND('',#2623,.T.);
#1770=FACE_OUTER_BOUND('',#2624,.T.);
#1771=FACE_OUTER_BOUND('',#2625,.T.);
#1772=FACE_OUTER_BOUND('',#2627,.T.);
#1773=FACE_OUTER_BOUND('',#2629,.T.);
#1774=FACE_OUTER_BOUND('',#2630,.T.);
#1775=FACE_OUTER_BOUND('',#2631,.T.);
#1776=FACE_OUTER_BOUND('',#2632,.T.);
#1777=FACE_OUTER_BOUND('',#2633,.T.);
#1778=FACE_OUTER_BOUND('',#2634,.T.);
#1779=FACE_OUTER_BOUND('',#2635,.T.);
#1780=FACE_OUTER_BOUND('',#2636,.T.);
#2466=EDGE_LOOP('',(#10213,#10214,#10215,#10216));
#2467=EDGE_LOOP('',(#10217,#10218,#10219,#10220,#10221,#10222));
#2468=EDGE_LOOP('',(#10223,#10224,#10225,#10226,#10227));
#2469=EDGE_LOOP('',(#10228,#10229,#10230,#10231,#10232));
#2470=EDGE_LOOP('',(#10233,#10234,#10235,#10236,#10237,#10238));
#2471=EDGE_LOOP('',(#10239,#10240,#10241,#10242));
#2472=EDGE_LOOP('',(#10243,#10244,#10245,#10246));
#2473=EDGE_LOOP('',(#10247,#10248,#10249,#10250));
#2474=EDGE_LOOP('',(#10251));
#2475=EDGE_LOOP('',(#10252));
#2476=EDGE_LOOP('',(#10253));
#2477=EDGE_LOOP('',(#10254));
#2478=EDGE_LOOP('',(#10255,#10256));
#2479=EDGE_LOOP('',(#10257,#10258));
#2480=EDGE_LOOP('',(#10259,#10260));
#2481=EDGE_LOOP('',(#10261,#10262));
#2482=EDGE_LOOP('',(#10263,#10264));
#2483=EDGE_LOOP('',(#10265,#10266));
#2484=EDGE_LOOP('',(#10267,#10268));
#2485=EDGE_LOOP('',(#10269,#10270,#10271,#10272,#10273));
#2486=EDGE_LOOP('',(#10274,#10275,#10276,#10277));
#2487=EDGE_LOOP('',(#10278,#10279,#10280,#10281));
#2488=EDGE_LOOP('',(#10282,#10283,#10284,#10285,#10286));
#2489=EDGE_LOOP('',(#10287,#10288,#10289,#10290));
#2490=EDGE_LOOP('',(#10291,#10292,#10293,#10294,#10295));
#2491=EDGE_LOOP('',(#10296,#10297,#10298,#10299,#10300));
#2492=EDGE_LOOP('',(#10301,#10302,#10303,#10304));
#2493=EDGE_LOOP('',(#10305,#10306,#10307,#10308));
#2494=EDGE_LOOP('',(#10309,#10310,#10311,#10312));
#2495=EDGE_LOOP('',(#10313,#10314,#10315,#10316));
#2496=EDGE_LOOP('',(#10317,#10318,#10319,#10320));
#2497=EDGE_LOOP('',(#10321,#10322,#10323,#10324,#10325));
#2498=EDGE_LOOP('',(#10326,#10327,#10328,#10329,#10330));
#2499=EDGE_LOOP('',(#10331));
#2500=EDGE_LOOP('',(#10332));
#2501=EDGE_LOOP('',(#10333));
#2502=EDGE_LOOP('',(#10334));
#2503=EDGE_LOOP('',(#10335));
#2504=EDGE_LOOP('',(#10336));
#2505=EDGE_LOOP('',(#10337));
#2506=EDGE_LOOP('',(#10338));
#2507=EDGE_LOOP('',(#10339));
#2508=EDGE_LOOP('',(#10340));
#2509=EDGE_LOOP('',(#10341));
#2510=EDGE_LOOP('',(#10342));
#2511=EDGE_LOOP('',(#10343,#10344,#10345,#10346));
#2512=EDGE_LOOP('',(#10347,#10348,#10349,#10350));
#2513=EDGE_LOOP('',(#10351,#10352,#10353,#10354));
#2514=EDGE_LOOP('',(#10355,#10356,#10357,#10358,#10359,#10360,#10361,#10362,
#10363,#10364,#10365,#10366));
#2515=EDGE_LOOP('',(#10367));
#2516=EDGE_LOOP('',(#10368));
#2517=EDGE_LOOP('',(#10369,#10370,#10371,#10372));
#2518=EDGE_LOOP('',(#10373,#10374,#10375,#10376));
#2519=EDGE_LOOP('',(#10377,#10378,#10379,#10380));
#2520=EDGE_LOOP('',(#10381,#10382,#10383,#10384,#10385,#10386,#10387,#10388,
#10389,#10390,#10391,#10392));
#2521=EDGE_LOOP('',(#10393));
#2522=EDGE_LOOP('',(#10394));
#2523=EDGE_LOOP('',(#10395,#10396,#10397,#10398));
#2524=EDGE_LOOP('',(#10399,#10400,#10401,#10402));
#2525=EDGE_LOOP('',(#10403,#10404,#10405,#10406));
#2526=EDGE_LOOP('',(#10407,#10408,#10409,#10410,#10411,#10412,#10413,#10414,
#10415,#10416,#10417,#10418));
#2527=EDGE_LOOP('',(#10419));
#2528=EDGE_LOOP('',(#10420));
#2529=EDGE_LOOP('',(#10421,#10422,#10423,#10424));
#2530=EDGE_LOOP('',(#10425,#10426,#10427,#10428));
#2531=EDGE_LOOP('',(#10429,#10430,#10431,#10432));
#2532=EDGE_LOOP('',(#10433,#10434,#10435,#10436,#10437,#10438,#10439,#10440,
#10441,#10442,#10443,#10444));
#2533=EDGE_LOOP('',(#10445));
#2534=EDGE_LOOP('',(#10446));
#2535=EDGE_LOOP('',(#10447,#10448,#10449,#10450));
#2536=EDGE_LOOP('',(#10451,#10452,#10453,#10454));
#2537=EDGE_LOOP('',(#10455,#10456,#10457,#10458));
#2538=EDGE_LOOP('',(#10459,#10460,#10461,#10462,#10463,#10464,#10465,#10466,
#10467,#10468,#10469,#10470));
#2539=EDGE_LOOP('',(#10471));
#2540=EDGE_LOOP('',(#10472));
#2541=EDGE_LOOP('',(#10473,#10474,#10475,#10476));
#2542=EDGE_LOOP('',(#10477,#10478,#10479,#10480));
#2543=EDGE_LOOP('',(#10481,#10482,#10483,#10484));
#2544=EDGE_LOOP('',(#10485,#10486,#10487,#10488,#10489,#10490,#10491,#10492,
#10493,#10494,#10495,#10496));
#2545=EDGE_LOOP('',(#10497));
#2546=EDGE_LOOP('',(#10498));
#2547=EDGE_LOOP('',(#10499,#10500,#10501,#10502,#10503,#10504,#10505,#10506,
#10507,#10508,#10509,#10510));
#2548=EDGE_LOOP('',(#10511));
#2549=EDGE_LOOP('',(#10512));
#2550=EDGE_LOOP('',(#10513,#10514,#10515,#10516));
#2551=EDGE_LOOP('',(#10517,#10518,#10519,#10520));
#2552=EDGE_LOOP('',(#10521,#10522,#10523,#10524));
#2553=EDGE_LOOP('',(#10525,#10526,#10527,#10528));
#2554=EDGE_LOOP('',(#10529,#10530,#10531,#10532));
#2555=EDGE_LOOP('',(#10533,#10534,#10535,#10536));
#2556=EDGE_LOOP('',(#10537,#10538,#10539,#10540));
#2557=EDGE_LOOP('',(#10541));
#2558=EDGE_LOOP('',(#10542));
#2559=EDGE_LOOP('',(#10543));
#2560=EDGE_LOOP('',(#10544));
#2561=EDGE_LOOP('',(#10545,#10546,#10547,#10548));
#2562=EDGE_LOOP('',(#10549,#10550,#10551,#10552,#10553,#10554));
#2563=EDGE_LOOP('',(#10555,#10556,#10557,#10558));
#2564=EDGE_LOOP('',(#10559,#10560,#10561,#10562));
#2565=EDGE_LOOP('',(#10563));
#2566=EDGE_LOOP('',(#10564));
#2567=EDGE_LOOP('',(#10565));
#2568=EDGE_LOOP('',(#10566));
#2569=EDGE_LOOP('',(#10567,#10568,#10569,#10570));
#2570=EDGE_LOOP('',(#10571,#10572,#10573,#10574));
#2571=EDGE_LOOP('',(#10575,#10576,#10577,#10578));
#2572=EDGE_LOOP('',(#10579,#10580,#10581,#10582));
#2573=EDGE_LOOP('',(#10583,#10584,#10585,#10586));
#2574=EDGE_LOOP('',(#10587,#10588,#10589,#10590));
#2575=EDGE_LOOP('',(#10591,#10592,#10593,#10594,#10595,#10596));
#2576=EDGE_LOOP('',(#10597,#10598,#10599,#10600));
#2577=EDGE_LOOP('',(#10601));
#2578=EDGE_LOOP('',(#10602));
#2579=EDGE_LOOP('',(#10603));
#2580=EDGE_LOOP('',(#10604));
#2581=EDGE_LOOP('',(#10605,#10606,#10607,#10608));
#2582=EDGE_LOOP('',(#10609,#10610,#10611,#10612));
#2583=EDGE_LOOP('',(#10613,#10614,#10615,#10616));
#2584=EDGE_LOOP('',(#10617,#10618,#10619,#10620));
#2585=EDGE_LOOP('',(#10621,#10622,#10623,#10624));
#2586=EDGE_LOOP('',(#10625,#10626,#10627,#10628));
#2587=EDGE_LOOP('',(#10629,#10630,#10631,#10632,#10633,#10634));
#2588=EDGE_LOOP('',(#10635,#10636,#10637,#10638));
#2589=EDGE_LOOP('',(#10639));
#2590=EDGE_LOOP('',(#10640));
#2591=EDGE_LOOP('',(#10641));
#2592=EDGE_LOOP('',(#10642));
#2593=EDGE_LOOP('',(#10643,#10644,#10645,#10646));
#2594=EDGE_LOOP('',(#10647,#10648,#10649,#10650));
#2595=EDGE_LOOP('',(#10651,#10652,#10653,#10654));
#2596=EDGE_LOOP('',(#10655,#10656,#10657,#10658));
#2597=EDGE_LOOP('',(#10659,#10660,#10661,#10662));
#2598=EDGE_LOOP('',(#10663,#10664,#10665,#10666));
#2599=EDGE_LOOP('',(#10667,#10668,#10669,#10670,#10671,#10672));
#2600=EDGE_LOOP('',(#10673,#10674,#10675,#10676));
#2601=EDGE_LOOP('',(#10677));
#2602=EDGE_LOOP('',(#10678));
#2603=EDGE_LOOP('',(#10679));
#2604=EDGE_LOOP('',(#10680));
#2605=EDGE_LOOP('',(#10681,#10682,#10683,#10684));
#2606=EDGE_LOOP('',(#10685,#10686,#10687,#10688));
#2607=EDGE_LOOP('',(#10689,#10690,#10691,#10692));
#2608=EDGE_LOOP('',(#10693,#10694,#10695,#10696));
#2609=EDGE_LOOP('',(#10697,#10698,#10699,#10700));
#2610=EDGE_LOOP('',(#10701,#10702,#10703,#10704));
#2611=EDGE_LOOP('',(#10705,#10706,#10707,#10708,#10709,#10710));
#2612=EDGE_LOOP('',(#10711,#10712,#10713,#10714));
#2613=EDGE_LOOP('',(#10715));
#2614=EDGE_LOOP('',(#10716));
#2615=EDGE_LOOP('',(#10717));
#2616=EDGE_LOOP('',(#10718));
#2617=EDGE_LOOP('',(#10719,#10720,#10721,#10722));
#2618=EDGE_LOOP('',(#10723,#10724,#10725,#10726));
#2619=EDGE_LOOP('',(#10727,#10728,#10729,#10730));
#2620=EDGE_LOOP('',(#10731,#10732,#10733,#10734));
#2621=EDGE_LOOP('',(#10735,#10736,#10737,#10738));
#2622=EDGE_LOOP('',(#10739,#10740,#10741,#10742));
#2623=EDGE_LOOP('',(#10743,#10744,#10745,#10746,#10747,#10748));
#2624=EDGE_LOOP('',(#10749,#10750,#10751,#10752));
#2625=EDGE_LOOP('',(#10753));
#2626=EDGE_LOOP('',(#10754));
#2627=EDGE_LOOP('',(#10755));
#2628=EDGE_LOOP('',(#10756));
#2629=EDGE_LOOP('',(#10757,#10758,#10759,#10760));
#2630=EDGE_LOOP('',(#10761,#10762,#10763,#10764));
#2631=EDGE_LOOP('',(#10765,#10766,#10767,#10768));
#2632=EDGE_LOOP('',(#10769,#10770,#10771,#10772));
#2633=EDGE_LOOP('',(#10773,#10774,#10775,#10776));
#2634=EDGE_LOOP('',(#10777,#10778,#10779,#10780,#10781,#10782));
#2635=EDGE_LOOP('',(#10783,#10784,#10785,#10786));
#2636=EDGE_LOOP('',(#10787,#10788,#10789,#10790));
#3381=LINE('',#39464,#3829);
#3382=LINE('',#39467,#3830);
#3383=LINE('',#39470,#3831);
#3384=LINE('',#39474,#3832);
#3385=LINE('',#39479,#3833);
#3386=LINE('',#39542,#3834);
#3387=LINE('',#39547,#3835);
#3388=LINE('',#39550,#3836);
#3389=LINE('',#39557,#3837);
#3390=LINE('',#39560,#3838);
#3391=LINE('',#39566,#3839);
#3392=LINE('',#39572,#3840);
#3393=LINE('',#39579,#3841);
#3394=LINE('',#39583,#3842);
#3829=VECTOR('',#16837,8.14999999999999);
#3830=VECTOR('',#16842,7.5);
#3831=VECTOR('',#16845,7.5);
#3832=VECTOR('',#16850,12.4653846153846);
#3833=VECTOR('',#16857,12.4653846153846);
#3834=VECTOR('',#16930,17.6897435897436);
#3835=VECTOR('',#16937,16.2686153846154);
#3836=VECTOR('',#16940,16.0346153846154);
#3837=VECTOR('',#16951,16.0346153846154);
#3838=VECTOR('',#16954,16.2686153846154);
#3839=VECTOR('',#16961,17.6897435897436);
#3840=VECTOR('',#16968,20.35);
#3841=VECTOR('',#16975,21.);
#3842=VECTOR('',#16982,21.);
#4338=CIRCLE('',#13942,12.4653846153846);
#4339=CIRCLE('',#13943,3.56616156686793);
#4340=CIRCLE('',#13944,12.4653846153846);
#4341=CIRCLE('',#13946,7.64278544417155);
#4342=CIRCLE('',#13947,7.64278544417155);
#4343=CIRCLE('',#13948,0.4875);
#4344=CIRCLE('',#13949,7.5);
#4345=CIRCLE('',#13950,7.5);
#4346=CIRCLE('',#13952,7.5);
#4347=CIRCLE('',#13953,7.5);
#4348=CIRCLE('',#13954,0.4875);
#4349=CIRCLE('',#13955,7.64278544417155);
#4350=CIRCLE('',#13957,8.14999999999999);
#4351=CIRCLE('',#13960,8.14999999999999);
#4352=CIRCLE('',#13962,12.4653846153846);
#4353=CIRCLE('',#13964,12.4653846153846);
#4354=CIRCLE('',#13968,3.56616156686793);
#4355=CIRCLE('',#13970,3.56616156686793);
#4356=CIRCLE('',#13972,3.56616156686793);
#4357=CIRCLE('',#13974,3.56616156686793);
#4358=CIRCLE('',#13976,3.56616156686793);
#4359=CIRCLE('',#13978,3.56616156686793);
#4360=CIRCLE('',#13980,3.56616156686793);
#4361=CIRCLE('',#13982,16.3271153846154);
#4362=CIRCLE('',#13983,0.0585);
#4363=CIRCLE('',#13984,16.2686153846154);
#4364=CIRCLE('',#13985,16.2686153846154);
#4365=CIRCLE('',#13987,16.0346153846154);
#4366=CIRCLE('',#13988,0.0585);
#4367=CIRCLE('',#13989,16.0931153846154);
#4368=CIRCLE('',#13991,16.3271153846154);
#4369=CIRCLE('',#13992,0.0585);
#4370=CIRCLE('',#13993,16.2686153846154);
#4371=CIRCLE('',#13995,16.0346153846154);
#4372=CIRCLE('',#13996,16.0346153846154);
#4373=CIRCLE('',#13997,0.0585);
#4374=CIRCLE('',#13998,16.0931153846154);
#4375=CIRCLE('',#14000,17.6897435897436);
#4376=CIRCLE('',#14001,17.6897435897436);
#4377=CIRCLE('',#14003,16.2686153846154);
#4378=CIRCLE('',#14005,16.0346153846154);
#4379=CIRCLE('',#14007,3.56616156686793);
#4380=CIRCLE('',#14008,16.0346153846154);
#4381=CIRCLE('',#14011,16.2686153846154);
#4382=CIRCLE('',#14013,17.6897435897436);
#4383=CIRCLE('',#14014,17.6897435897436);
#4384=CIRCLE('',#14016,21.);
#4385=CIRCLE('',#14017,20.35);
#4386=CIRCLE('',#14019,21.);
#4387=CIRCLE('',#14020,20.35);
#4388=CIRCLE('',#14021,21.);
#4389=CIRCLE('',#14030,3.96060240207311);
#4390=CIRCLE('',#14031,1.69469015025);
#4391=CIRCLE('',#14032,3.96060240207311);
#4392=CIRCLE('',#14034,3.39763111739558);
#4393=CIRCLE('',#14035,3.56616156686792);
#4394=CIRCLE('',#14036,3.39763111739558);
#4395=CIRCLE('',#14037,3.39763111739558);
#4396=CIRCLE('',#14038,3.39763111739558);
#4397=CIRCLE('',#14039,3.39763111739558);
#4398=CIRCLE('',#14040,3.39763111739558);
#4399=CIRCLE('',#14041,3.45272288248773);
#4400=CIRCLE('',#14042,3.45272288248773);
#4401=CIRCLE('',#14044,3.96060240207311);
#4402=CIRCLE('',#14045,1.69469015025);
#4403=CIRCLE('',#14046,3.96060240207311);
#4404=CIRCLE('',#14048,3.39763111739558);
#4405=CIRCLE('',#14049,3.56616156686792);
#4406=CIRCLE('',#14050,3.39763111739558);
#4407=CIRCLE('',#14051,3.39763111739558);
#4408=CIRCLE('',#14052,3.39763111739558);
#4409=CIRCLE('',#14053,3.39763111739558);
#4410=CIRCLE('',#14054,3.39763111739558);
#4411=CIRCLE('',#14055,3.45272288248773);
#4412=CIRCLE('',#14056,3.45272288248773);
#4413=CIRCLE('',#14058,3.96060240207311);
#4414=CIRCLE('',#14059,1.69469015025);
#4415=CIRCLE('',#14060,3.96060240207311);
#4416=CIRCLE('',#14062,3.39763111739558);
#4417=CIRCLE('',#14063,3.56616156686792);
#4418=CIRCLE('',#14064,3.39763111739558);
#4419=CIRCLE('',#14065,3.39763111739558);
#4420=CIRCLE('',#14066,3.39763111739558);
#4421=CIRCLE('',#14067,3.39763111739558);
#4422=CIRCLE('',#14068,3.39763111739558);
#4423=CIRCLE('',#14069,3.45272288248773);
#4424=CIRCLE('',#14070,3.45272288248773);
#4425=CIRCLE('',#14072,3.96060240207311);
#4426=CIRCLE('',#14073,1.69469015025);
#4427=CIRCLE('',#14074,3.96060240207311);
#4428=CIRCLE('',#14076,3.39763111739558);
#4429=CIRCLE('',#14077,3.56616156686792);
#4430=CIRCLE('',#14078,3.39763111739558);
#4431=CIRCLE('',#14079,3.39763111739558);
#4432=CIRCLE('',#14080,3.39763111739558);
#4433=CIRCLE('',#14081,3.39763111739558);
#4434=CIRCLE('',#14082,3.39763111739558);
#4435=CIRCLE('',#14083,3.45272288248773);
#4436=CIRCLE('',#14084,3.45272288248773);
#4437=CIRCLE('',#14086,3.96060240207311);
#4438=CIRCLE('',#14087,1.69469015025);
#4439=CIRCLE('',#14088,3.96060240207311);
#4440=CIRCLE('',#14090,3.39763111739558);
#4441=CIRCLE('',#14091,3.56616156686792);
#4442=CIRCLE('',#14092,3.39763111739558);
#4443=CIRCLE('',#14093,3.39763111739558);
#4444=CIRCLE('',#14094,3.39763111739558);
#4445=CIRCLE('',#14095,3.39763111739558);
#4446=CIRCLE('',#14096,3.39763111739558);
#4447=CIRCLE('',#14097,3.45272288248773);
#4448=CIRCLE('',#14098,3.45272288248773);
#4449=CIRCLE('',#14100,3.96060240207311);
#4450=CIRCLE('',#14101,1.69469015025);
#4451=CIRCLE('',#14102,3.96060240207311);
#4452=CIRCLE('',#14104,3.39763111739558);
#4453=CIRCLE('',#14105,3.39763111739558);
#4454=CIRCLE('',#14106,3.39763111739558);
#4455=CIRCLE('',#14107,3.56616156686792);
#4456=CIRCLE('',#14108,3.39763111739558);
#4457=CIRCLE('',#14109,3.39763111739558);
#4458=CIRCLE('',#14110,3.39763111739558);
#4459=CIRCLE('',#14111,3.45272288248773);
#4460=CIRCLE('',#14112,3.45272288248773);
#4461=CIRCLE('',#14114,3.39763111739558);
#4462=CIRCLE('',#14115,3.56616156686792);
#4463=CIRCLE('',#14116,3.39763111739558);
#4464=CIRCLE('',#14117,3.39763111739558);
#4465=CIRCLE('',#14118,3.39763111739558);
#4466=CIRCLE('',#14119,3.39763111739558);
#4467=CIRCLE('',#14120,3.39763111739558);
#4468=CIRCLE('',#14121,3.45272288248773);
#4469=CIRCLE('',#14122,3.45272288248773);
#4470=CIRCLE('',#14124,3.96060240207311);
#4471=CIRCLE('',#14125,1.69469015025);
#4472=CIRCLE('',#14126,3.96060240207311);
#4473=CIRCLE('',#14128,14.25);
#4474=CIRCLE('',#14129,14.25);
#4475=CIRCLE('',#14131,15.1423076923077);
#4476=CIRCLE('',#14132,15.1423076923077);
#4477=CIRCLE('',#14138,14.25);
#4478=CIRCLE('',#14139,15.1423076923077);
#4479=CIRCLE('',#14141,14.25);
#4480=CIRCLE('',#14142,15.1423076923077);
#4481=CIRCLE('',#14148,14.25);
#4482=CIRCLE('',#14149,15.1423076923077);
#4483=CIRCLE('',#14151,14.25);
#4484=CIRCLE('',#14152,15.1423076923077);
#4485=CIRCLE('',#14156,14.25);
#4486=CIRCLE('',#14157,14.25);
#4487=CIRCLE('',#14159,15.1423076923077);
#4488=CIRCLE('',#14160,15.1423076923077);
#4489=CIRCLE('',#14166,14.25);
#4490=CIRCLE('',#14167,15.1423076923077);
#4491=CIRCLE('',#14169,14.25);
#4492=CIRCLE('',#14170,15.1423076923077);
#4493=CIRCLE('',#14174,14.25);
#4494=CIRCLE('',#14175,14.25);
#4495=CIRCLE('',#14177,15.1423076923077);
#4496=CIRCLE('',#14178,15.1423076923077);
#4497=CIRCLE('',#14184,14.25);
#4498=CIRCLE('',#14185,15.1423076923077);
#4499=CIRCLE('',#14187,14.25);
#4500=CIRCLE('',#14188,15.1423076923077);
#4501=CIRCLE('',#14192,14.25);
#4502=CIRCLE('',#14193,14.25);
#4503=CIRCLE('',#14195,15.1423076923077);
#4504=CIRCLE('',#14196,15.1423076923077);
#4505=CIRCLE('',#14202,14.25);
#4506=CIRCLE('',#14203,15.1423076923077);
#4507=CIRCLE('',#14205,14.25);
#4508=CIRCLE('',#14206,15.1423076923077);
#4509=CIRCLE('',#14210,14.25);
#4510=CIRCLE('',#14211,14.25);
#4511=CIRCLE('',#14213,15.1423076923077);
#4512=CIRCLE('',#14214,15.1423076923077);
#4513=CIRCLE('',#14220,14.25);
#4514=CIRCLE('',#14221,15.1423076923077);
#4515=CIRCLE('',#14223,14.25);
#4516=CIRCLE('',#14224,15.1423076923077);
#4517=CIRCLE('',#14228,14.25);
#4518=CIRCLE('',#14229,14.25);
#4519=CIRCLE('',#14231,15.1423076923077);
#4520=CIRCLE('',#14232,15.1423076923077);
#4521=CIRCLE('',#14238,14.25);
#4522=CIRCLE('',#14239,15.1423076923077);
#4523=CIRCLE('',#14241,14.25);
#4524=CIRCLE('',#14242,15.1423076923077);
#4525=CIRCLE('',#14246,14.25);
#4526=CIRCLE('',#14247,15.1423076923077);
#4527=CIRCLE('',#14249,14.25);
#4528=CIRCLE('',#14250,15.1423076923077);
#5611=VERTEX_POINT('',#39439);
#5612=VERTEX_POINT('',#39441);
#5613=VERTEX_POINT('',#39445);
#5614=VERTEX_POINT('',#39446);
#5615=VERTEX_POINT('',#39449);
#5616=VERTEX_POINT('',#39451);
#5617=VERTEX_POINT('',#39455);
#5618=VERTEX_POINT('',#39456);
#5619=VERTEX_POINT('',#39459);
#5620=VERTEX_POINT('',#39463);
#5621=VERTEX_POINT('',#39469);
#5622=VERTEX_POINT('',#39473);
#5623=VERTEX_POINT('',#39477);
#5624=VERTEX_POINT('',#39483);
#5625=VERTEX_POINT('',#39484);
#5626=VERTEX_POINT('',#39487);
#5627=VERTEX_POINT('',#39488);
#5628=VERTEX_POINT('',#39491);
#5629=VERTEX_POINT('',#39492);
#5630=VERTEX_POINT('',#39495);
#5631=VERTEX_POINT('',#39496);
#5632=VERTEX_POINT('',#39499);
#5633=VERTEX_POINT('',#39500);
#5634=VERTEX_POINT('',#39503);
#5635=VERTEX_POINT('',#39504);
#5636=VERTEX_POINT('',#39507);
#5637=VERTEX_POINT('',#39508);
#5638=VERTEX_POINT('',#39511);
#5639=VERTEX_POINT('',#39513);
#5640=VERTEX_POINT('',#39515);
#5641=VERTEX_POINT('',#39519);
#5642=VERTEX_POINT('',#39521);
#5643=VERTEX_POINT('',#39525);
#5644=VERTEX_POINT('',#39527);
#5645=VERTEX_POINT('',#39531);
#5646=VERTEX_POINT('',#39532);
#5647=VERTEX_POINT('',#39535);
#5648=VERTEX_POINT('',#39539);
#5649=VERTEX_POINT('',#39541);
#5650=VERTEX_POINT('',#39545);
#5651=VERTEX_POINT('',#39549);
#5652=VERTEX_POINT('',#39553);
#5653=VERTEX_POINT('',#39559);
#5654=VERTEX_POINT('',#39563);
#5655=VERTEX_POINT('',#39565);
#5656=VERTEX_POINT('',#39569);
#5657=VERTEX_POINT('',#39571);
#5658=VERTEX_POINT('',#39575);
#5659=VERTEX_POINT('',#39576);
#5660=VERTEX_POINT('',#39578);
#5661=VERTEX_POINT('',#39591);
#5662=VERTEX_POINT('',#39593);
#5663=VERTEX_POINT('',#39596);
#5664=VERTEX_POINT('',#39597);
#5665=VERTEX_POINT('',#39604);
#5666=VERTEX_POINT('',#39624);
#5667=VERTEX_POINT('',#39650);
#5668=VERTEX_POINT('',#39651);
#5669=VERTEX_POINT('',#39658);
#5670=VERTEX_POINT('',#39678);
#5671=VERTEX_POINT('',#39705);
#5672=VERTEX_POINT('',#39706);
#5673=VERTEX_POINT('',#39708);
#5674=VERTEX_POINT('',#39710);
#5675=VERTEX_POINT('',#39712);
#5676=VERTEX_POINT('',#39720);
#5677=VERTEX_POINT('',#39722);
#5678=VERTEX_POINT('',#39731);
#5679=VERTEX_POINT('',#39733);
#5680=VERTEX_POINT('',#39740);
#5681=VERTEX_POINT('',#39748);
#5682=VERTEX_POINT('',#39750);
#5683=VERTEX_POINT('',#39753);
#5684=VERTEX_POINT('',#39755);
#5685=VERTEX_POINT('',#39758);
#5686=VERTEX_POINT('',#39759);
#5687=VERTEX_POINT('',#39766);
#5688=VERTEX_POINT('',#39786);
#5689=VERTEX_POINT('',#39812);
#5690=VERTEX_POINT('',#39813);
#5691=VERTEX_POINT('',#39820);
#5692=VERTEX_POINT('',#39840);
#5693=VERTEX_POINT('',#39867);
#5694=VERTEX_POINT('',#39868);
#5695=VERTEX_POINT('',#39870);
#5696=VERTEX_POINT('',#39872);
#5697=VERTEX_POINT('',#39874);
#5698=VERTEX_POINT('',#39882);
#5699=VERTEX_POINT('',#39884);
#5700=VERTEX_POINT('',#39893);
#5701=VERTEX_POINT('',#39895);
#5702=VERTEX_POINT('',#39902);
#5703=VERTEX_POINT('',#39910);
#5704=VERTEX_POINT('',#39912);
#5705=VERTEX_POINT('',#39915);
#5706=VERTEX_POINT('',#39917);
#5707=VERTEX_POINT('',#39920);
#5708=VERTEX_POINT('',#39921);
#5709=VERTEX_POINT('',#39928);
#5710=VERTEX_POINT('',#39948);
#5711=VERTEX_POINT('',#39974);
#5712=VERTEX_POINT('',#39975);
#5713=VERTEX_POINT('',#39982);
#5714=VERTEX_POINT('',#40002);
#5715=VERTEX_POINT('',#40029);
#5716=VERTEX_POINT('',#40030);
#5717=VERTEX_POINT('',#40032);
#5718=VERTEX_POINT('',#40034);
#5719=VERTEX_POINT('',#40036);
#5720=VERTEX_POINT('',#40044);
#5721=VERTEX_POINT('',#40046);
#5722=VERTEX_POINT('',#40055);
#5723=VERTEX_POINT('',#40057);
#5724=VERTEX_POINT('',#40064);
#5725=VERTEX_POINT('',#40072);
#5726=VERTEX_POINT('',#40074);
#5727=VERTEX_POINT('',#40077);
#5728=VERTEX_POINT('',#40079);
#5729=VERTEX_POINT('',#40082);
#5730=VERTEX_POINT('',#40083);
#5731=VERTEX_POINT('',#40090);
#5732=VERTEX_POINT('',#40110);
#5733=VERTEX_POINT('',#40136);
#5734=VERTEX_POINT('',#40137);
#5735=VERTEX_POINT('',#40144);
#5736=VERTEX_POINT('',#40164);
#5737=VERTEX_POINT('',#40191);
#5738=VERTEX_POINT('',#40192);
#5739=VERTEX_POINT('',#40194);
#5740=VERTEX_POINT('',#40196);
#5741=VERTEX_POINT('',#40198);
#5742=VERTEX_POINT('',#40206);
#5743=VERTEX_POINT('',#40208);
#5744=VERTEX_POINT('',#40217);
#5745=VERTEX_POINT('',#40219);
#5746=VERTEX_POINT('',#40226);
#5747=VERTEX_POINT('',#40234);
#5748=VERTEX_POINT('',#40236);
#5749=VERTEX_POINT('',#40239);
#5750=VERTEX_POINT('',#40241);
#5751=VERTEX_POINT('',#40244);
#5752=VERTEX_POINT('',#40245);
#5753=VERTEX_POINT('',#40252);
#5754=VERTEX_POINT('',#40272);
#5755=VERTEX_POINT('',#40298);
#5756=VERTEX_POINT('',#40299);
#5757=VERTEX_POINT('',#40306);
#5758=VERTEX_POINT('',#40326);
#5759=VERTEX_POINT('',#40353);
#5760=VERTEX_POINT('',#40354);
#5761=VERTEX_POINT('',#40356);
#5762=VERTEX_POINT('',#40358);
#5763=VERTEX_POINT('',#40360);
#5764=VERTEX_POINT('',#40368);
#5765=VERTEX_POINT('',#40370);
#5766=VERTEX_POINT('',#40379);
#5767=VERTEX_POINT('',#40381);
#5768=VERTEX_POINT('',#40388);
#5769=VERTEX_POINT('',#40396);
#5770=VERTEX_POINT('',#40398);
#5771=VERTEX_POINT('',#40401);
#5772=VERTEX_POINT('',#40403);
#5773=VERTEX_POINT('',#40406);
#5774=VERTEX_POINT('',#40407);
#5775=VERTEX_POINT('',#40427);
#5776=VERTEX_POINT('',#40434);
#5777=VERTEX_POINT('',#40460);
#5778=VERTEX_POINT('',#40461);
#5779=VERTEX_POINT('',#40468);
#5780=VERTEX_POINT('',#40488);
#5781=VERTEX_POINT('',#40515);
#5782=VERTEX_POINT('',#40516);
#5783=VERTEX_POINT('',#40518);
#5784=VERTEX_POINT('',#40525);
#5785=VERTEX_POINT('',#40527);
#5786=VERTEX_POINT('',#40535);
#5787=VERTEX_POINT('',#40537);
#5788=VERTEX_POINT('',#40539);
#5789=VERTEX_POINT('',#40547);
#5790=VERTEX_POINT('',#40549);
#5791=VERTEX_POINT('',#40558);
#5792=VERTEX_POINT('',#40560);
#5793=VERTEX_POINT('',#40563);
#5794=VERTEX_POINT('',#40564);
#5795=VERTEX_POINT('',#40566);
#5796=VERTEX_POINT('',#40568);
#5797=VERTEX_POINT('',#40570);
#5798=VERTEX_POINT('',#40578);
#5799=VERTEX_POINT('',#40580);
#5800=VERTEX_POINT('',#40589);
#5801=VERTEX_POINT('',#40591);
#5802=VERTEX_POINT('',#40598);
#5803=VERTEX_POINT('',#40606);
#5804=VERTEX_POINT('',#40608);
#5805=VERTEX_POINT('',#40611);
#5806=VERTEX_POINT('',#40613);
#5807=VERTEX_POINT('',#40616);
#5808=VERTEX_POINT('',#40617);
#5809=VERTEX_POINT('',#40624);
#5810=VERTEX_POINT('',#40644);
#5811=VERTEX_POINT('',#40670);
#5812=VERTEX_POINT('',#40671);
#5813=VERTEX_POINT('',#40678);
#5814=VERTEX_POINT('',#40698);
#7268=EDGE_CURVE('',#5611,#5611,#4338,.T.);
#7269=EDGE_CURVE('',#5611,#5612,#4339,.T.);
#7270=EDGE_CURVE('',#5612,#5612,#4340,.T.);
#7271=EDGE_CURVE('',#5613,#5614,#4341,.T.);
#7272=EDGE_CURVE('',#5614,#5613,#4342,.T.);
#7273=EDGE_CURVE('',#5614,#5615,#4343,.T.);
#7274=EDGE_CURVE('',#5616,#5615,#4344,.T.);
#7275=EDGE_CURVE('',#5615,#5616,#4345,.T.);
#7276=EDGE_CURVE('',#5617,#5618,#4346,.T.);
#7277=EDGE_CURVE('',#5618,#5617,#4347,.T.);
#7278=EDGE_CURVE('',#5618,#5619,#4348,.T.);
#7279=EDGE_CURVE('',#5619,#5619,#4349,.T.);
#7280=EDGE_CURVE('',#5613,#5620,#3381,.T.);
#7281=EDGE_CURVE('',#5620,#5620,#4350,.T.);
#7282=EDGE_CURVE('',#5617,#5616,#3382,.T.);
#7283=EDGE_CURVE('',#5619,#5621,#3383,.T.);
#7284=EDGE_CURVE('',#5621,#5621,#4351,.T.);
#7285=EDGE_CURVE('',#5612,#5622,#3384,.T.);
#7286=EDGE_CURVE('',#5622,#5622,#4352,.T.);
#7287=EDGE_CURVE('',#5623,#5623,#4353,.T.);
#7288=EDGE_CURVE('',#5623,#5611,#3385,.T.);
#7289=EDGE_CURVE('',#5624,#5625,#4354,.T.);
#7290=EDGE_CURVE('',#5626,#5627,#4355,.T.);
#7291=EDGE_CURVE('',#5628,#5629,#4356,.T.);
#7292=EDGE_CURVE('',#5630,#5631,#4357,.T.);
#7293=EDGE_CURVE('',#5632,#5633,#4358,.T.);
#7294=EDGE_CURVE('',#5634,#5635,#4359,.T.);
#7295=EDGE_CURVE('',#5636,#5637,#4360,.T.);
#7296=EDGE_CURVE('',#5638,#5638,#4361,.T.);
#7297=EDGE_CURVE('',#5638,#5639,#4362,.T.);
#7298=EDGE_CURVE('',#5640,#5639,#4363,.T.);
#7299=EDGE_CURVE('',#5639,#5640,#4364,.T.);
#7300=EDGE_CURVE('',#5641,#5641,#4365,.T.);
#7301=EDGE_CURVE('',#5641,#5642,#4366,.T.);
#7302=EDGE_CURVE('',#5642,#5642,#4367,.T.);
#7303=EDGE_CURVE('',#5643,#5643,#4368,.T.);
#7304=EDGE_CURVE('',#5643,#5644,#4369,.T.);
#7305=EDGE_CURVE('',#5644,#5644,#4370,.T.);
#7306=EDGE_CURVE('',#5645,#5646,#4371,.T.);
#7307=EDGE_CURVE('',#5646,#5645,#4372,.T.);
#7308=EDGE_CURVE('',#5646,#5647,#4373,.T.);
#7309=EDGE_CURVE('',#5647,#5647,#4374,.T.);
#7310=EDGE_CURVE('',#5648,#5648,#4375,.T.);
#7311=EDGE_CURVE('',#5648,#5649,#3386,.T.);
#7312=EDGE_CURVE('',#5649,#5649,#4376,.T.);
#7313=EDGE_CURVE('',#5650,#5650,#4377,.T.);
#7314=EDGE_CURVE('',#5650,#5640,#3387,.T.);
#7315=EDGE_CURVE('',#5645,#5651,#3388,.T.);
#7316=EDGE_CURVE('',#5651,#5651,#4378,.T.);
#7317=EDGE_CURVE('',#5651,#5652,#4379,.T.);
#7318=EDGE_CURVE('',#5652,#5652,#4380,.T.);
#7319=EDGE_CURVE('',#5652,#5641,#3389,.T.);
#7320=EDGE_CURVE('',#5644,#5653,#3390,.T.);
#7321=EDGE_CURVE('',#5653,#5653,#4381,.T.);
#7322=EDGE_CURVE('',#5654,#5654,#4382,.T.);
#7323=EDGE_CURVE('',#5654,#5655,#3391,.T.);
#7324=EDGE_CURVE('',#5655,#5655,#4383,.T.);
#7325=EDGE_CURVE('',#5656,#5656,#4384,.T.);
#7326=EDGE_CURVE('',#5656,#5657,#3392,.T.);
#7327=EDGE_CURVE('',#5657,#5657,#4385,.T.);
#7328=EDGE_CURVE('',#5658,#5659,#4386,.T.);
#7329=EDGE_CURVE('',#5659,#5660,#3393,.T.);
#7330=EDGE_CURVE('',#5660,#5660,#4387,.T.);
#7331=EDGE_CURVE('',#5659,#5658,#4388,.T.);
#7332=EDGE_CURVE('',#5658,#5656,#3394,.T.);
#7333=EDGE_CURVE('',#5661,#5661,#4389,.T.);
#7334=EDGE_CURVE('',#5661,#5662,#4390,.T.);
#7335=EDGE_CURVE('',#5662,#5662,#4391,.T.);
#7336=EDGE_CURVE('',#5663,#5664,#695,.T.);
#7337=EDGE_CURVE('',#5663,#5665,#696,.T.);
#7338=EDGE_CURVE('',#5665,#5666,#697,.T.);
#7339=EDGE_CURVE('',#5666,#5664,#698,.T.);
#7340=EDGE_CURVE('',#5667,#5668,#699,.T.);
#7341=EDGE_CURVE('',#5667,#5669,#700,.T.);
#7342=EDGE_CURVE('',#5669,#5670,#701,.T.);
#7343=EDGE_CURVE('',#5670,#5668,#702,.T.);
#7344=EDGE_CURVE('',#5671,#5672,#4392,.T.);
#7345=EDGE_CURVE('',#5672,#5673,#4393,.T.);
#7346=EDGE_CURVE('',#5673,#5674,#4394,.T.);
#7347=EDGE_CURVE('',#5674,#5675,#703,.T.);
#7348=EDGE_CURVE('',#5676,#5675,#4395,.T.);
#7349=EDGE_CURVE('',#5676,#5677,#704,.T.);
#7350=EDGE_CURVE('',#5677,#5673,#4396,.T.);
#7351=EDGE_CURVE('',#5672,#5678,#4397,.T.);
#7352=EDGE_CURVE('',#5678,#5679,#705,.T.);
#7353=EDGE_CURVE('',#5680,#5679,#4398,.T.);
#7354=EDGE_CURVE('',#5680,#5671,#706,.T.);
#7355=EDGE_CURVE('',#5681,#5681,#4399,.T.);
#7356=EDGE_CURVE('',#5682,#5682,#4400,.T.);
#7357=EDGE_CURVE('',#5683,#5683,#4401,.T.);
#7358=EDGE_CURVE('',#5683,#5684,#4402,.T.);
#7359=EDGE_CURVE('',#5684,#5684,#4403,.T.);
#7360=EDGE_CURVE('',#5685,#5686,#707,.T.);
#7361=EDGE_CURVE('',#5685,#5687,#708,.T.);
#7362=EDGE_CURVE('',#5687,#5688,#709,.T.);
#7363=EDGE_CURVE('',#5688,#5686,#710,.T.);
#7364=EDGE_CURVE('',#5689,#5690,#711,.T.);
#7365=EDGE_CURVE('',#5689,#5691,#712,.T.);
#7366=EDGE_CURVE('',#5691,#5692,#713,.T.);
#7367=EDGE_CURVE('',#5692,#5690,#714,.T.);
#7368=EDGE_CURVE('',#5693,#5694,#4404,.T.);
#7369=EDGE_CURVE('',#5694,#5695,#4405,.T.);
#7370=EDGE_CURVE('',#5695,#5696,#4406,.T.);
#7371=EDGE_CURVE('',#5696,#5697,#715,.T.);
#7372=EDGE_CURVE('',#5698,#5697,#4407,.T.);
#7373=EDGE_CURVE('',#5698,#5699,#716,.T.);
#7374=EDGE_CURVE('',#5699,#5695,#4408,.T.);
#7375=EDGE_CURVE('',#5694,#5700,#4409,.T.);
#7376=EDGE_CURVE('',#5700,#5701,#717,.T.);
#7377=EDGE_CURVE('',#5702,#5701,#4410,.T.);
#7378=EDGE_CURVE('',#5702,#5693,#718,.T.);
#7379=EDGE_CURVE('',#5703,#5703,#4411,.T.);
#7380=EDGE_CURVE('',#5704,#5704,#4412,.T.);
#7381=EDGE_CURVE('',#5705,#5705,#4413,.T.);
#7382=EDGE_CURVE('',#5705,#5706,#4414,.T.);
#7383=EDGE_CURVE('',#5706,#5706,#4415,.T.);
#7384=EDGE_CURVE('',#5707,#5708,#719,.T.);
#7385=EDGE_CURVE('',#5707,#5709,#720,.T.);
#7386=EDGE_CURVE('',#5709,#5710,#721,.T.);
#7387=EDGE_CURVE('',#5710,#5708,#722,.T.);
#7388=EDGE_CURVE('',#5711,#5712,#723,.T.);
#7389=EDGE_CURVE('',#5711,#5713,#724,.T.);
#7390=EDGE_CURVE('',#5713,#5714,#725,.T.);
#7391=EDGE_CURVE('',#5714,#5712,#726,.T.);
#7392=EDGE_CURVE('',#5715,#5716,#4416,.T.);
#7393=EDGE_CURVE('',#5716,#5717,#4417,.T.);
#7394=EDGE_CURVE('',#5717,#5718,#4418,.T.);
#7395=EDGE_CURVE('',#5718,#5719,#727,.T.);
#7396=EDGE_CURVE('',#5720,#5719,#4419,.T.);
#7397=EDGE_CURVE('',#5720,#5721,#728,.T.);
#7398=EDGE_CURVE('',#5721,#5717,#4420,.T.);
#7399=EDGE_CURVE('',#5716,#5722,#4421,.T.);
#7400=EDGE_CURVE('',#5722,#5723,#729,.T.);
#7401=EDGE_CURVE('',#5724,#5723,#4422,.T.);
#7402=EDGE_CURVE('',#5724,#5715,#730,.T.);
#7403=EDGE_CURVE('',#5725,#5725,#4423,.T.);
#7404=EDGE_CURVE('',#5726,#5726,#4424,.T.);
#7405=EDGE_CURVE('',#5727,#5727,#4425,.T.);
#7406=EDGE_CURVE('',#5727,#5728,#4426,.T.);
#7407=EDGE_CURVE('',#5728,#5728,#4427,.T.);
#7408=EDGE_CURVE('',#5729,#5730,#731,.T.);
#7409=EDGE_CURVE('',#5729,#5731,#732,.T.);
#7410=EDGE_CURVE('',#5731,#5732,#733,.T.);
#7411=EDGE_CURVE('',#5732,#5730,#734,.T.);
#7412=EDGE_CURVE('',#5733,#5734,#735,.T.);
#7413=EDGE_CURVE('',#5733,#5735,#736,.T.);
#7414=EDGE_CURVE('',#5735,#5736,#737,.T.);
#7415=EDGE_CURVE('',#5736,#5734,#738,.T.);
#7416=EDGE_CURVE('',#5737,#5738,#4428,.T.);
#7417=EDGE_CURVE('',#5738,#5739,#4429,.T.);
#7418=EDGE_CURVE('',#5739,#5740,#4430,.T.);
#7419=EDGE_CURVE('',#5740,#5741,#739,.T.);
#7420=EDGE_CURVE('',#5742,#5741,#4431,.T.);
#7421=EDGE_CURVE('',#5742,#5743,#740,.T.);
#7422=EDGE_CURVE('',#5743,#5739,#4432,.T.);
#7423=EDGE_CURVE('',#5738,#5744,#4433,.T.);
#7424=EDGE_CURVE('',#5744,#5745,#741,.T.);
#7425=EDGE_CURVE('',#5746,#5745,#4434,.T.);
#7426=EDGE_CURVE('',#5746,#5737,#742,.T.);
#7427=EDGE_CURVE('',#5747,#5747,#4435,.T.);
#7428=EDGE_CURVE('',#5748,#5748,#4436,.T.);
#7429=EDGE_CURVE('',#5749,#5749,#4437,.T.);
#7430=EDGE_CURVE('',#5749,#5750,#4438,.T.);
#7431=EDGE_CURVE('',#5750,#5750,#4439,.T.);
#7432=EDGE_CURVE('',#5751,#5752,#743,.T.);
#7433=EDGE_CURVE('',#5751,#5753,#744,.T.);
#7434=EDGE_CURVE('',#5753,#5754,#745,.T.);
#7435=EDGE_CURVE('',#5754,#5752,#746,.T.);
#7436=EDGE_CURVE('',#5755,#5756,#747,.T.);
#7437=EDGE_CURVE('',#5755,#5757,#748,.T.);
#7438=EDGE_CURVE('',#5757,#5758,#749,.T.);
#7439=EDGE_CURVE('',#5758,#5756,#750,.T.);
#7440=EDGE_CURVE('',#5759,#5760,#4440,.T.);
#7441=EDGE_CURVE('',#5760,#5761,#4441,.T.);
#7442=EDGE_CURVE('',#5761,#5762,#4442,.T.);
#7443=EDGE_CURVE('',#5762,#5763,#751,.T.);
#7444=EDGE_CURVE('',#5764,#5763,#4443,.T.);
#7445=EDGE_CURVE('',#5764,#5765,#752,.T.);
#7446=EDGE_CURVE('',#5765,#5761,#4444,.T.);
#7447=EDGE_CURVE('',#5760,#5766,#4445,.T.);
#7448=EDGE_CURVE('',#5766,#5767,#753,.T.);
#7449=EDGE_CURVE('',#5768,#5767,#4446,.T.);
#7450=EDGE_CURVE('',#5768,#5759,#754,.T.);
#7451=EDGE_CURVE('',#5769,#5769,#4447,.T.);
#7452=EDGE_CURVE('',#5770,#5770,#4448,.T.);
#7453=EDGE_CURVE('',#5771,#5771,#4449,.T.);
#7454=EDGE_CURVE('',#5771,#5772,#4450,.T.);
#7455=EDGE_CURVE('',#5772,#5772,#4451,.T.);
#7456=EDGE_CURVE('',#5773,#5774,#755,.T.);
#7457=EDGE_CURVE('',#5773,#5775,#756,.T.);
#7458=EDGE_CURVE('',#5776,#5775,#757,.T.);
#7459=EDGE_CURVE('',#5774,#5776,#758,.T.);
#7460=EDGE_CURVE('',#5777,#5778,#759,.T.);
#7461=EDGE_CURVE('',#5777,#5779,#760,.T.);
#7462=EDGE_CURVE('',#5779,#5780,#761,.T.);
#7463=EDGE_CURVE('',#5780,#5778,#762,.T.);
#7464=EDGE_CURVE('',#5781,#5782,#4452,.T.);
#7465=EDGE_CURVE('',#5783,#5781,#763,.T.);
#7466=EDGE_CURVE('',#5783,#5784,#4453,.T.);
#7467=EDGE_CURVE('',#5785,#5784,#764,.T.);
#7468=EDGE_CURVE('',#5782,#5785,#4454,.T.);
#7469=EDGE_CURVE('',#5782,#5786,#4455,.T.);
#7470=EDGE_CURVE('',#5786,#5787,#4456,.T.);
#7471=EDGE_CURVE('',#5787,#5788,#765,.T.);
#7472=EDGE_CURVE('',#5789,#5788,#4457,.T.);
#7473=EDGE_CURVE('',#5789,#5790,#766,.T.);
#7474=EDGE_CURVE('',#5790,#5786,#4458,.T.);
#7475=EDGE_CURVE('',#5791,#5791,#4459,.T.);
#7476=EDGE_CURVE('',#5792,#5792,#4460,.T.);
#7477=EDGE_CURVE('',#5793,#5794,#4461,.T.);
#7478=EDGE_CURVE('',#5794,#5795,#4462,.T.);
#7479=EDGE_CURVE('',#5795,#5796,#4463,.T.);
#7480=EDGE_CURVE('',#5796,#5797,#767,.T.);
#7481=EDGE_CURVE('',#5798,#5797,#4464,.T.);
#7482=EDGE_CURVE('',#5798,#5799,#768,.T.);
#7483=EDGE_CURVE('',#5799,#5795,#4465,.T.);
#7484=EDGE_CURVE('',#5794,#5800,#4466,.T.);
#7485=EDGE_CURVE('',#5800,#5801,#769,.T.);
#7486=EDGE_CURVE('',#5802,#5801,#4467,.T.);
#7487=EDGE_CURVE('',#5802,#5793,#770,.T.);
#7488=EDGE_CURVE('',#5803,#5803,#4468,.T.);
#7489=EDGE_CURVE('',#5804,#5804,#4469,.T.);
#7490=EDGE_CURVE('',#5805,#5805,#4470,.T.);
#7491=EDGE_CURVE('',#5805,#5806,#4471,.T.);
#7492=EDGE_CURVE('',#5806,#5806,#4472,.T.);
#7493=EDGE_CURVE('',#5807,#5808,#771,.T.);
#7494=EDGE_CURVE('',#5807,#5809,#772,.T.);
#7495=EDGE_CURVE('',#5809,#5810,#773,.T.);
#7496=EDGE_CURVE('',#5810,#5808,#774,.T.);
#7497=EDGE_CURVE('',#5811,#5812,#775,.T.);
#7498=EDGE_CURVE('',#5811,#5813,#776,.T.);
#7499=EDGE_CURVE('',#5813,#5814,#777,.T.);
#7500=EDGE_CURVE('',#5814,#5812,#778,.T.);
#7501=EDGE_CURVE('',#5814,#5776,#4473,.T.);
#7502=EDGE_CURVE('',#5812,#5775,#4474,.T.);
#7503=EDGE_CURVE('',#5773,#5811,#4475,.T.);
#7504=EDGE_CURVE('',#5774,#5813,#4476,.T.);
#7505=EDGE_CURVE('',#5801,#5798,#4477,.T.);
#7506=EDGE_CURVE('',#5797,#5802,#4478,.T.);
#7507=EDGE_CURVE('',#5800,#5799,#4479,.T.);
#7508=EDGE_CURVE('',#5796,#5793,#4480,.T.);
#7509=EDGE_CURVE('',#5780,#5753,#4481,.T.);
#7510=EDGE_CURVE('',#5754,#5779,#4482,.T.);
#7511=EDGE_CURVE('',#5778,#5751,#4483,.T.);
#7512=EDGE_CURVE('',#5752,#5777,#4484,.T.);
#7513=EDGE_CURVE('',#5767,#5764,#4485,.T.);
#7514=EDGE_CURVE('',#5766,#5765,#4486,.T.);
#7515=EDGE_CURVE('',#5762,#5759,#4487,.T.);
#7516=EDGE_CURVE('',#5763,#5768,#4488,.T.);
#7517=EDGE_CURVE('',#5758,#5731,#4489,.T.);
#7518=EDGE_CURVE('',#5732,#5757,#4490,.T.);
#7519=EDGE_CURVE('',#5756,#5729,#4491,.T.);
#7520=EDGE_CURVE('',#5730,#5755,#4492,.T.);
#7521=EDGE_CURVE('',#5745,#5742,#4493,.T.);
#7522=EDGE_CURVE('',#5744,#5743,#4494,.T.);
#7523=EDGE_CURVE('',#5740,#5737,#4495,.T.);
#7524=EDGE_CURVE('',#5741,#5746,#4496,.T.);
#7525=EDGE_CURVE('',#5736,#5709,#4497,.T.);
#7526=EDGE_CURVE('',#5710,#5735,#4498,.T.);
#7527=EDGE_CURVE('',#5734,#5707,#4499,.T.);
#7528=EDGE_CURVE('',#5708,#5733,#4500,.T.);
#7529=EDGE_CURVE('',#5723,#5720,#4501,.T.);
#7530=EDGE_CURVE('',#5722,#5721,#4502,.T.);
#7531=EDGE_CURVE('',#5718,#5715,#4503,.T.);
#7532=EDGE_CURVE('',#5719,#5724,#4504,.T.);
#7533=EDGE_CURVE('',#5714,#5687,#4505,.T.);
#7534=EDGE_CURVE('',#5688,#5713,#4506,.T.);
#7535=EDGE_CURVE('',#5712,#5685,#4507,.T.);
#7536=EDGE_CURVE('',#5686,#5711,#4508,.T.);
#7537=EDGE_CURVE('',#5701,#5698,#4509,.T.);
#7538=EDGE_CURVE('',#5700,#5699,#4510,.T.);
#7539=EDGE_CURVE('',#5696,#5693,#4511,.T.);
#7540=EDGE_CURVE('',#5697,#5702,#4512,.T.);
#7541=EDGE_CURVE('',#5692,#5665,#4513,.T.);
#7542=EDGE_CURVE('',#5666,#5691,#4514,.T.);
#7543=EDGE_CURVE('',#5690,#5663,#4515,.T.);
#7544=EDGE_CURVE('',#5664,#5689,#4516,.T.);
#7545=EDGE_CURVE('',#5679,#5676,#4517,.T.);
#7546=EDGE_CURVE('',#5678,#5677,#4518,.T.);
#7547=EDGE_CURVE('',#5674,#5671,#4519,.T.);
#7548=EDGE_CURVE('',#5675,#5680,#4520,.T.);
#7549=EDGE_CURVE('',#5670,#5809,#4521,.T.);
#7550=EDGE_CURVE('',#5810,#5669,#4522,.T.);
#7551=EDGE_CURVE('',#5668,#5807,#4523,.T.);
#7552=EDGE_CURVE('',#5808,#5667,#4524,.T.);
#7553=EDGE_CURVE('',#5783,#5789,#4525,.T.);
#7554=EDGE_CURVE('',#5788,#5784,#4526,.T.);
#7555=EDGE_CURVE('',#5781,#5790,#4527,.T.);
#7556=EDGE_CURVE('',#5787,#5785,#4528,.T.);
#10213=ORIENTED_EDGE('',*,*,#7268,.F.);
#10214=ORIENTED_EDGE('',*,*,#7269,.T.);
#10215=ORIENTED_EDGE('',*,*,#7270,.T.);
#10216=ORIENTED_EDGE('',*,*,#7269,.F.);
#10217=ORIENTED_EDGE('',*,*,#7271,.F.);
#10218=ORIENTED_EDGE('',*,*,#7272,.F.);
#10219=ORIENTED_EDGE('',*,*,#7273,.T.);
#10220=ORIENTED_EDGE('',*,*,#7274,.F.);
#10221=ORIENTED_EDGE('',*,*,#7275,.F.);
#10222=ORIENTED_EDGE('',*,*,#7273,.F.);
#10223=ORIENTED_EDGE('',*,*,#7276,.F.);
#10224=ORIENTED_EDGE('',*,*,#7277,.F.);
#10225=ORIENTED_EDGE('',*,*,#7278,.T.);
#10226=ORIENTED_EDGE('',*,*,#7279,.F.);
#10227=ORIENTED_EDGE('',*,*,#7278,.F.);
#10228=ORIENTED_EDGE('',*,*,#7271,.T.);
#10229=ORIENTED_EDGE('',*,*,#7272,.T.);
#10230=ORIENTED_EDGE('',*,*,#7280,.T.);
#10231=ORIENTED_EDGE('',*,*,#7281,.T.);
#10232=ORIENTED_EDGE('',*,*,#7280,.F.);
#10233=ORIENTED_EDGE('',*,*,#7276,.T.);
#10234=ORIENTED_EDGE('',*,*,#7277,.T.);
#10235=ORIENTED_EDGE('',*,*,#7282,.T.);
#10236=ORIENTED_EDGE('',*,*,#7274,.T.);
#10237=ORIENTED_EDGE('',*,*,#7275,.T.);
#10238=ORIENTED_EDGE('',*,*,#7282,.F.);
#10239=ORIENTED_EDGE('',*,*,#7279,.T.);
#10240=ORIENTED_EDGE('',*,*,#7283,.T.);
#10241=ORIENTED_EDGE('',*,*,#7284,.F.);
#10242=ORIENTED_EDGE('',*,*,#7283,.F.);
#10243=ORIENTED_EDGE('',*,*,#7270,.F.);
#10244=ORIENTED_EDGE('',*,*,#7285,.T.);
#10245=ORIENTED_EDGE('',*,*,#7286,.T.);
#10246=ORIENTED_EDGE('',*,*,#7285,.F.);
#10247=ORIENTED_EDGE('',*,*,#7287,.F.);
#10248=ORIENTED_EDGE('',*,*,#7288,.T.);
#10249=ORIENTED_EDGE('',*,*,#7268,.T.);
#10250=ORIENTED_EDGE('',*,*,#7288,.F.);
#10251=ORIENTED_EDGE('',*,*,#7287,.T.);
#10252=ORIENTED_EDGE('',*,*,#7281,.F.);
#10253=ORIENTED_EDGE('',*,*,#7286,.F.);
#10254=ORIENTED_EDGE('',*,*,#7284,.T.);
#10255=ORIENTED_EDGE('',*,*,#7289,.T.);
#10256=ORIENTED_EDGE('',*,*,#7289,.F.);
#10257=ORIENTED_EDGE('',*,*,#7290,.T.);
#10258=ORIENTED_EDGE('',*,*,#7290,.F.);
#10259=ORIENTED_EDGE('',*,*,#7291,.T.);
#10260=ORIENTED_EDGE('',*,*,#7291,.F.);
#10261=ORIENTED_EDGE('',*,*,#7292,.T.);
#10262=ORIENTED_EDGE('',*,*,#7292,.F.);
#10263=ORIENTED_EDGE('',*,*,#7293,.T.);
#10264=ORIENTED_EDGE('',*,*,#7293,.F.);
#10265=ORIENTED_EDGE('',*,*,#7294,.T.);
#10266=ORIENTED_EDGE('',*,*,#7294,.F.);
#10267=ORIENTED_EDGE('',*,*,#7295,.T.);
#10268=ORIENTED_EDGE('',*,*,#7295,.F.);
#10269=ORIENTED_EDGE('',*,*,#7296,.F.);
#10270=ORIENTED_EDGE('',*,*,#7297,.T.);
#10271=ORIENTED_EDGE('',*,*,#7298,.F.);
#10272=ORIENTED_EDGE('',*,*,#7299,.F.);
#10273=ORIENTED_EDGE('',*,*,#7297,.F.);
#10274=ORIENTED_EDGE('',*,*,#7300,.F.);
#10275=ORIENTED_EDGE('',*,*,#7301,.T.);
#10276=ORIENTED_EDGE('',*,*,#7302,.F.);
#10277=ORIENTED_EDGE('',*,*,#7301,.F.);
#10278=ORIENTED_EDGE('',*,*,#7303,.F.);
#10279=ORIENTED_EDGE('',*,*,#7304,.T.);
#10280=ORIENTED_EDGE('',*,*,#7305,.F.);
#10281=ORIENTED_EDGE('',*,*,#7304,.F.);
#10282=ORIENTED_EDGE('',*,*,#7306,.F.);
#10283=ORIENTED_EDGE('',*,*,#7307,.F.);
#10284=ORIENTED_EDGE('',*,*,#7308,.T.);
#10285=ORIENTED_EDGE('',*,*,#7309,.F.);
#10286=ORIENTED_EDGE('',*,*,#7308,.F.);
#10287=ORIENTED_EDGE('',*,*,#7310,.F.);
#10288=ORIENTED_EDGE('',*,*,#7311,.T.);
#10289=ORIENTED_EDGE('',*,*,#7312,.T.);
#10290=ORIENTED_EDGE('',*,*,#7311,.F.);
#10291=ORIENTED_EDGE('',*,*,#7313,.F.);
#10292=ORIENTED_EDGE('',*,*,#7314,.T.);
#10293=ORIENTED_EDGE('',*,*,#7298,.T.);
#10294=ORIENTED_EDGE('',*,*,#7299,.T.);
#10295=ORIENTED_EDGE('',*,*,#7314,.F.);
#10296=ORIENTED_EDGE('',*,*,#7306,.T.);
#10297=ORIENTED_EDGE('',*,*,#7307,.T.);
#10298=ORIENTED_EDGE('',*,*,#7315,.T.);
#10299=ORIENTED_EDGE('',*,*,#7316,.T.);
#10300=ORIENTED_EDGE('',*,*,#7315,.F.);
#10301=ORIENTED_EDGE('',*,*,#7316,.F.);
#10302=ORIENTED_EDGE('',*,*,#7317,.T.);
#10303=ORIENTED_EDGE('',*,*,#7318,.T.);
#10304=ORIENTED_EDGE('',*,*,#7317,.F.);
#10305=ORIENTED_EDGE('',*,*,#7318,.F.);
#10306=ORIENTED_EDGE('',*,*,#7319,.T.);
#10307=ORIENTED_EDGE('',*,*,#7300,.T.);
#10308=ORIENTED_EDGE('',*,*,#7319,.F.);
#10309=ORIENTED_EDGE('',*,*,#7305,.T.);
#10310=ORIENTED_EDGE('',*,*,#7320,.T.);
#10311=ORIENTED_EDGE('',*,*,#7321,.T.);
#10312=ORIENTED_EDGE('',*,*,#7320,.F.);
#10313=ORIENTED_EDGE('',*,*,#7322,.F.);
#10314=ORIENTED_EDGE('',*,*,#7323,.T.);
#10315=ORIENTED_EDGE('',*,*,#7324,.T.);
#10316=ORIENTED_EDGE('',*,*,#7323,.F.);
#10317=ORIENTED_EDGE('',*,*,#7325,.F.);
#10318=ORIENTED_EDGE('',*,*,#7326,.T.);
#10319=ORIENTED_EDGE('',*,*,#7327,.T.);
#10320=ORIENTED_EDGE('',*,*,#7326,.F.);
#10321=ORIENTED_EDGE('',*,*,#7328,.T.);
#10322=ORIENTED_EDGE('',*,*,#7329,.T.);
#10323=ORIENTED_EDGE('',*,*,#7330,.F.);
#10324=ORIENTED_EDGE('',*,*,#7329,.F.);
#10325=ORIENTED_EDGE('',*,*,#7331,.T.);
#10326=ORIENTED_EDGE('',*,*,#7328,.F.);
#10327=ORIENTED_EDGE('',*,*,#7332,.T.);
#10328=ORIENTED_EDGE('',*,*,#7325,.T.);
#10329=ORIENTED_EDGE('',*,*,#7332,.F.);
#10330=ORIENTED_EDGE('',*,*,#7331,.F.);
#10331=ORIENTED_EDGE('',*,*,#7330,.T.);
#10332=ORIENTED_EDGE('',*,*,#7296,.T.);
#10333=ORIENTED_EDGE('',*,*,#7327,.F.);
#10334=ORIENTED_EDGE('',*,*,#7303,.T.);
#10335=ORIENTED_EDGE('',*,*,#7324,.F.);
#10336=ORIENTED_EDGE('',*,*,#7309,.T.);
#10337=ORIENTED_EDGE('',*,*,#7322,.T.);
#10338=ORIENTED_EDGE('',*,*,#7321,.F.);
#10339=ORIENTED_EDGE('',*,*,#7312,.F.);
#10340=ORIENTED_EDGE('',*,*,#7313,.T.);
#10341=ORIENTED_EDGE('',*,*,#7310,.T.);
#10342=ORIENTED_EDGE('',*,*,#7302,.T.);
#10343=ORIENTED_EDGE('',*,*,#7333,.F.);
#10344=ORIENTED_EDGE('',*,*,#7334,.T.);
#10345=ORIENTED_EDGE('',*,*,#7335,.T.);
#10346=ORIENTED_EDGE('',*,*,#7334,.F.);
#10347=ORIENTED_EDGE('',*,*,#7336,.F.);
#10348=ORIENTED_EDGE('',*,*,#7337,.T.);
#10349=ORIENTED_EDGE('',*,*,#7338,.T.);
#10350=ORIENTED_EDGE('',*,*,#7339,.T.);
#10351=ORIENTED_EDGE('',*,*,#7340,.F.);
#10352=ORIENTED_EDGE('',*,*,#7341,.T.);
#10353=ORIENTED_EDGE('',*,*,#7342,.T.);
#10354=ORIENTED_EDGE('',*,*,#7343,.T.);
#10355=ORIENTED_EDGE('',*,*,#7344,.T.);
#10356=ORIENTED_EDGE('',*,*,#7345,.T.);
#10357=ORIENTED_EDGE('',*,*,#7346,.T.);
#10358=ORIENTED_EDGE('',*,*,#7347,.T.);
#10359=ORIENTED_EDGE('',*,*,#7348,.F.);
#10360=ORIENTED_EDGE('',*,*,#7349,.T.);
#10361=ORIENTED_EDGE('',*,*,#7350,.T.);
#10362=ORIENTED_EDGE('',*,*,#7345,.F.);
#10363=ORIENTED_EDGE('',*,*,#7351,.T.);
#10364=ORIENTED_EDGE('',*,*,#7352,.T.);
#10365=ORIENTED_EDGE('',*,*,#7353,.F.);
#10366=ORIENTED_EDGE('',*,*,#7354,.T.);
#10367=ORIENTED_EDGE('',*,*,#7355,.F.);
#10368=ORIENTED_EDGE('',*,*,#7356,.T.);
#10369=ORIENTED_EDGE('',*,*,#7357,.F.);
#10370=ORIENTED_EDGE('',*,*,#7358,.T.);
#10371=ORIENTED_EDGE('',*,*,#7359,.T.);
#10372=ORIENTED_EDGE('',*,*,#7358,.F.);
#10373=ORIENTED_EDGE('',*,*,#7360,.F.);
#10374=ORIENTED_EDGE('',*,*,#7361,.T.);
#10375=ORIENTED_EDGE('',*,*,#7362,.T.);
#10376=ORIENTED_EDGE('',*,*,#7363,.T.);
#10377=ORIENTED_EDGE('',*,*,#7364,.F.);
#10378=ORIENTED_EDGE('',*,*,#7365,.T.);
#10379=ORIENTED_EDGE('',*,*,#7366,.T.);
#10380=ORIENTED_EDGE('',*,*,#7367,.T.);
#10381=ORIENTED_EDGE('',*,*,#7368,.T.);
#10382=ORIENTED_EDGE('',*,*,#7369,.T.);
#10383=ORIENTED_EDGE('',*,*,#7370,.T.);
#10384=ORIENTED_EDGE('',*,*,#7371,.T.);
#10385=ORIENTED_EDGE('',*,*,#7372,.F.);
#10386=ORIENTED_EDGE('',*,*,#7373,.T.);
#10387=ORIENTED_EDGE('',*,*,#7374,.T.);
#10388=ORIENTED_EDGE('',*,*,#7369,.F.);
#10389=ORIENTED_EDGE('',*,*,#7375,.T.);
#10390=ORIENTED_EDGE('',*,*,#7376,.T.);
#10391=ORIENTED_EDGE('',*,*,#7377,.F.);
#10392=ORIENTED_EDGE('',*,*,#7378,.T.);
#10393=ORIENTED_EDGE('',*,*,#7379,.F.);
#10394=ORIENTED_EDGE('',*,*,#7380,.T.);
#10395=ORIENTED_EDGE('',*,*,#7381,.F.);
#10396=ORIENTED_EDGE('',*,*,#7382,.T.);
#10397=ORIENTED_EDGE('',*,*,#7383,.T.);
#10398=ORIENTED_EDGE('',*,*,#7382,.F.);
#10399=ORIENTED_EDGE('',*,*,#7384,.F.);
#10400=ORIENTED_EDGE('',*,*,#7385,.T.);
#10401=ORIENTED_EDGE('',*,*,#7386,.T.);
#10402=ORIENTED_EDGE('',*,*,#7387,.T.);
#10403=ORIENTED_EDGE('',*,*,#7388,.F.);
#10404=ORIENTED_EDGE('',*,*,#7389,.T.);
#10405=ORIENTED_EDGE('',*,*,#7390,.T.);
#10406=ORIENTED_EDGE('',*,*,#7391,.T.);
#10407=ORIENTED_EDGE('',*,*,#7392,.T.);
#10408=ORIENTED_EDGE('',*,*,#7393,.T.);
#10409=ORIENTED_EDGE('',*,*,#7394,.T.);
#10410=ORIENTED_EDGE('',*,*,#7395,.T.);
#10411=ORIENTED_EDGE('',*,*,#7396,.F.);
#10412=ORIENTED_EDGE('',*,*,#7397,.T.);
#10413=ORIENTED_EDGE('',*,*,#7398,.T.);
#10414=ORIENTED_EDGE('',*,*,#7393,.F.);
#10415=ORIENTED_EDGE('',*,*,#7399,.T.);
#10416=ORIENTED_EDGE('',*,*,#7400,.T.);
#10417=ORIENTED_EDGE('',*,*,#7401,.F.);
#10418=ORIENTED_EDGE('',*,*,#7402,.T.);
#10419=ORIENTED_EDGE('',*,*,#7403,.F.);
#10420=ORIENTED_EDGE('',*,*,#7404,.T.);
#10421=ORIENTED_EDGE('',*,*,#7405,.F.);
#10422=ORIENTED_EDGE('',*,*,#7406,.T.);
#10423=ORIENTED_EDGE('',*,*,#7407,.T.);
#10424=ORIENTED_EDGE('',*,*,#7406,.F.);
#10425=ORIENTED_EDGE('',*,*,#7408,.F.);
#10426=ORIENTED_EDGE('',*,*,#7409,.T.);
#10427=ORIENTED_EDGE('',*,*,#7410,.T.);
#10428=ORIENTED_EDGE('',*,*,#7411,.T.);
#10429=ORIENTED_EDGE('',*,*,#7412,.F.);
#10430=ORIENTED_EDGE('',*,*,#7413,.T.);
#10431=ORIENTED_EDGE('',*,*,#7414,.T.);
#10432=ORIENTED_EDGE('',*,*,#7415,.T.);
#10433=ORIENTED_EDGE('',*,*,#7416,.T.);
#10434=ORIENTED_EDGE('',*,*,#7417,.T.);
#10435=ORIENTED_EDGE('',*,*,#7418,.T.);
#10436=ORIENTED_EDGE('',*,*,#7419,.T.);
#10437=ORIENTED_EDGE('',*,*,#7420,.F.);
#10438=ORIENTED_EDGE('',*,*,#7421,.T.);
#10439=ORIENTED_EDGE('',*,*,#7422,.T.);
#10440=ORIENTED_EDGE('',*,*,#7417,.F.);
#10441=ORIENTED_EDGE('',*,*,#7423,.T.);
#10442=ORIENTED_EDGE('',*,*,#7424,.T.);
#10443=ORIENTED_EDGE('',*,*,#7425,.F.);
#10444=ORIENTED_EDGE('',*,*,#7426,.T.);
#10445=ORIENTED_EDGE('',*,*,#7427,.F.);
#10446=ORIENTED_EDGE('',*,*,#7428,.T.);
#10447=ORIENTED_EDGE('',*,*,#7429,.F.);
#10448=ORIENTED_EDGE('',*,*,#7430,.T.);
#10449=ORIENTED_EDGE('',*,*,#7431,.T.);
#10450=ORIENTED_EDGE('',*,*,#7430,.F.);
#10451=ORIENTED_EDGE('',*,*,#7432,.F.);
#10452=ORIENTED_EDGE('',*,*,#7433,.T.);
#10453=ORIENTED_EDGE('',*,*,#7434,.T.);
#10454=ORIENTED_EDGE('',*,*,#7435,.T.);
#10455=ORIENTED_EDGE('',*,*,#7436,.F.);
#10456=ORIENTED_EDGE('',*,*,#7437,.T.);
#10457=ORIENTED_EDGE('',*,*,#7438,.T.);
#10458=ORIENTED_EDGE('',*,*,#7439,.T.);
#10459=ORIENTED_EDGE('',*,*,#7440,.T.);
#10460=ORIENTED_EDGE('',*,*,#7441,.T.);
#10461=ORIENTED_EDGE('',*,*,#7442,.T.);
#10462=ORIENTED_EDGE('',*,*,#7443,.T.);
#10463=ORIENTED_EDGE('',*,*,#7444,.F.);
#10464=ORIENTED_EDGE('',*,*,#7445,.T.);
#10465=ORIENTED_EDGE('',*,*,#7446,.T.);
#10466=ORIENTED_EDGE('',*,*,#7441,.F.);
#10467=ORIENTED_EDGE('',*,*,#7447,.T.);
#10468=ORIENTED_EDGE('',*,*,#7448,.T.);
#10469=ORIENTED_EDGE('',*,*,#7449,.F.);
#10470=ORIENTED_EDGE('',*,*,#7450,.T.);
#10471=ORIENTED_EDGE('',*,*,#7451,.F.);
#10472=ORIENTED_EDGE('',*,*,#7452,.T.);
#10473=ORIENTED_EDGE('',*,*,#7453,.F.);
#10474=ORIENTED_EDGE('',*,*,#7454,.T.);
#10475=ORIENTED_EDGE('',*,*,#7455,.T.);
#10476=ORIENTED_EDGE('',*,*,#7454,.F.);
#10477=ORIENTED_EDGE('',*,*,#7456,.F.);
#10478=ORIENTED_EDGE('',*,*,#7457,.T.);
#10479=ORIENTED_EDGE('',*,*,#7458,.F.);
#10480=ORIENTED_EDGE('',*,*,#7459,.F.);
#10481=ORIENTED_EDGE('',*,*,#7460,.F.);
#10482=ORIENTED_EDGE('',*,*,#7461,.T.);
#10483=ORIENTED_EDGE('',*,*,#7462,.T.);
#10484=ORIENTED_EDGE('',*,*,#7463,.T.);
#10485=ORIENTED_EDGE('',*,*,#7464,.F.);
#10486=ORIENTED_EDGE('',*,*,#7465,.F.);
#10487=ORIENTED_EDGE('',*,*,#7466,.T.);
#10488=ORIENTED_EDGE('',*,*,#7467,.F.);
#10489=ORIENTED_EDGE('',*,*,#7468,.F.);
#10490=ORIENTED_EDGE('',*,*,#7469,.T.);
#10491=ORIENTED_EDGE('',*,*,#7470,.T.);
#10492=ORIENTED_EDGE('',*,*,#7471,.T.);
#10493=ORIENTED_EDGE('',*,*,#7472,.F.);
#10494=ORIENTED_EDGE('',*,*,#7473,.T.);
#10495=ORIENTED_EDGE('',*,*,#7474,.T.);
#10496=ORIENTED_EDGE('',*,*,#7469,.F.);
#10497=ORIENTED_EDGE('',*,*,#7475,.F.);
#10498=ORIENTED_EDGE('',*,*,#7476,.T.);
#10499=ORIENTED_EDGE('',*,*,#7477,.T.);
#10500=ORIENTED_EDGE('',*,*,#7478,.T.);
#10501=ORIENTED_EDGE('',*,*,#7479,.T.);
#10502=ORIENTED_EDGE('',*,*,#7480,.T.);
#10503=ORIENTED_EDGE('',*,*,#7481,.F.);
#10504=ORIENTED_EDGE('',*,*,#7482,.T.);
#10505=ORIENTED_EDGE('',*,*,#7483,.T.);
#10506=ORIENTED_EDGE('',*,*,#7478,.F.);
#10507=ORIENTED_EDGE('',*,*,#7484,.T.);
#10508=ORIENTED_EDGE('',*,*,#7485,.T.);
#10509=ORIENTED_EDGE('',*,*,#7486,.F.);
#10510=ORIENTED_EDGE('',*,*,#7487,.T.);
#10511=ORIENTED_EDGE('',*,*,#7488,.F.);
#10512=ORIENTED_EDGE('',*,*,#7489,.T.);
#10513=ORIENTED_EDGE('',*,*,#7490,.F.);
#10514=ORIENTED_EDGE('',*,*,#7491,.T.);
#10515=ORIENTED_EDGE('',*,*,#7492,.T.);
#10516=ORIENTED_EDGE('',*,*,#7491,.F.);
#10517=ORIENTED_EDGE('',*,*,#7493,.F.);
#10518=ORIENTED_EDGE('',*,*,#7494,.T.);
#10519=ORIENTED_EDGE('',*,*,#7495,.T.);
#10520=ORIENTED_EDGE('',*,*,#7496,.T.);
#10521=ORIENTED_EDGE('',*,*,#7497,.F.);
#10522=ORIENTED_EDGE('',*,*,#7498,.T.);
#10523=ORIENTED_EDGE('',*,*,#7499,.T.);
#10524=ORIENTED_EDGE('',*,*,#7500,.T.);
#10525=ORIENTED_EDGE('',*,*,#7501,.T.);
#10526=ORIENTED_EDGE('',*,*,#7458,.T.);
#10527=ORIENTED_EDGE('',*,*,#7502,.F.);
#10528=ORIENTED_EDGE('',*,*,#7500,.F.);
#10529=ORIENTED_EDGE('',*,*,#7503,.F.);
#10530=ORIENTED_EDGE('',*,*,#7456,.T.);
#10531=ORIENTED_EDGE('',*,*,#7504,.T.);
#10532=ORIENTED_EDGE('',*,*,#7498,.F.);
#10533=ORIENTED_EDGE('',*,*,#7457,.F.);
#10534=ORIENTED_EDGE('',*,*,#7503,.T.);
#10535=ORIENTED_EDGE('',*,*,#7497,.T.);
#10536=ORIENTED_EDGE('',*,*,#7502,.T.);
#10537=ORIENTED_EDGE('',*,*,#7504,.F.);
#10538=ORIENTED_EDGE('',*,*,#7459,.T.);
#10539=ORIENTED_EDGE('',*,*,#7501,.F.);
#10540=ORIENTED_EDGE('',*,*,#7499,.F.);
#10541=ORIENTED_EDGE('',*,*,#7490,.T.);
#10542=ORIENTED_EDGE('',*,*,#7489,.F.);
#10543=ORIENTED_EDGE('',*,*,#7492,.F.);
#10544=ORIENTED_EDGE('',*,*,#7488,.T.);
#10545=ORIENTED_EDGE('',*,*,#7505,.T.);
#10546=ORIENTED_EDGE('',*,*,#7481,.T.);
#10547=ORIENTED_EDGE('',*,*,#7506,.T.);
#10548=ORIENTED_EDGE('',*,*,#7486,.T.);
#10549=ORIENTED_EDGE('',*,*,#7483,.F.);
#10550=ORIENTED_EDGE('',*,*,#7507,.F.);
#10551=ORIENTED_EDGE('',*,*,#7484,.F.);
#10552=ORIENTED_EDGE('',*,*,#7477,.F.);
#10553=ORIENTED_EDGE('',*,*,#7508,.F.);
#10554=ORIENTED_EDGE('',*,*,#7479,.F.);
#10555=ORIENTED_EDGE('',*,*,#7480,.F.);
#10556=ORIENTED_EDGE('',*,*,#7508,.T.);
#10557=ORIENTED_EDGE('',*,*,#7487,.F.);
#10558=ORIENTED_EDGE('',*,*,#7506,.F.);
#10559=ORIENTED_EDGE('',*,*,#7482,.F.);
#10560=ORIENTED_EDGE('',*,*,#7505,.F.);
#10561=ORIENTED_EDGE('',*,*,#7485,.F.);
#10562=ORIENTED_EDGE('',*,*,#7507,.T.);
#10563=ORIENTED_EDGE('',*,*,#7455,.F.);
#10564=ORIENTED_EDGE('',*,*,#7475,.T.);
#10565=ORIENTED_EDGE('',*,*,#7453,.T.);
#10566=ORIENTED_EDGE('',*,*,#7476,.F.);
#10567=ORIENTED_EDGE('',*,*,#7434,.F.);
#10568=ORIENTED_EDGE('',*,*,#7509,.F.);
#10569=ORIENTED_EDGE('',*,*,#7462,.F.);
#10570=ORIENTED_EDGE('',*,*,#7510,.F.);
#10571=ORIENTED_EDGE('',*,*,#7511,.T.);
#10572=ORIENTED_EDGE('',*,*,#7432,.T.);
#10573=ORIENTED_EDGE('',*,*,#7512,.T.);
#10574=ORIENTED_EDGE('',*,*,#7460,.T.);
#10575=ORIENTED_EDGE('',*,*,#7435,.F.);
#10576=ORIENTED_EDGE('',*,*,#7510,.T.);
#10577=ORIENTED_EDGE('',*,*,#7461,.F.);
#10578=ORIENTED_EDGE('',*,*,#7512,.F.);
#10579=ORIENTED_EDGE('',*,*,#7433,.F.);
#10580=ORIENTED_EDGE('',*,*,#7511,.F.);
#10581=ORIENTED_EDGE('',*,*,#7463,.F.);
#10582=ORIENTED_EDGE('',*,*,#7509,.T.);
#10583=ORIENTED_EDGE('',*,*,#7445,.F.);
#10584=ORIENTED_EDGE('',*,*,#7513,.F.);
#10585=ORIENTED_EDGE('',*,*,#7448,.F.);
#10586=ORIENTED_EDGE('',*,*,#7514,.T.);
#10587=ORIENTED_EDGE('',*,*,#7443,.F.);
#10588=ORIENTED_EDGE('',*,*,#7515,.T.);
#10589=ORIENTED_EDGE('',*,*,#7450,.F.);
#10590=ORIENTED_EDGE('',*,*,#7516,.F.);
#10591=ORIENTED_EDGE('',*,*,#7446,.F.);
#10592=ORIENTED_EDGE('',*,*,#7514,.F.);
#10593=ORIENTED_EDGE('',*,*,#7447,.F.);
#10594=ORIENTED_EDGE('',*,*,#7440,.F.);
#10595=ORIENTED_EDGE('',*,*,#7515,.F.);
#10596=ORIENTED_EDGE('',*,*,#7442,.F.);
#10597=ORIENTED_EDGE('',*,*,#7513,.T.);
#10598=ORIENTED_EDGE('',*,*,#7444,.T.);
#10599=ORIENTED_EDGE('',*,*,#7516,.T.);
#10600=ORIENTED_EDGE('',*,*,#7449,.T.);
#10601=ORIENTED_EDGE('',*,*,#7431,.F.);
#10602=ORIENTED_EDGE('',*,*,#7451,.T.);
#10603=ORIENTED_EDGE('',*,*,#7429,.T.);
#10604=ORIENTED_EDGE('',*,*,#7452,.F.);
#10605=ORIENTED_EDGE('',*,*,#7410,.F.);
#10606=ORIENTED_EDGE('',*,*,#7517,.F.);
#10607=ORIENTED_EDGE('',*,*,#7438,.F.);
#10608=ORIENTED_EDGE('',*,*,#7518,.F.);
#10609=ORIENTED_EDGE('',*,*,#7519,.T.);
#10610=ORIENTED_EDGE('',*,*,#7408,.T.);
#10611=ORIENTED_EDGE('',*,*,#7520,.T.);
#10612=ORIENTED_EDGE('',*,*,#7436,.T.);
#10613=ORIENTED_EDGE('',*,*,#7411,.F.);
#10614=ORIENTED_EDGE('',*,*,#7518,.T.);
#10615=ORIENTED_EDGE('',*,*,#7437,.F.);
#10616=ORIENTED_EDGE('',*,*,#7520,.F.);
#10617=ORIENTED_EDGE('',*,*,#7409,.F.);
#10618=ORIENTED_EDGE('',*,*,#7519,.F.);
#10619=ORIENTED_EDGE('',*,*,#7439,.F.);
#10620=ORIENTED_EDGE('',*,*,#7517,.T.);
#10621=ORIENTED_EDGE('',*,*,#7421,.F.);
#10622=ORIENTED_EDGE('',*,*,#7521,.F.);
#10623=ORIENTED_EDGE('',*,*,#7424,.F.);
#10624=ORIENTED_EDGE('',*,*,#7522,.T.);
#10625=ORIENTED_EDGE('',*,*,#7419,.F.);
#10626=ORIENTED_EDGE('',*,*,#7523,.T.);
#10627=ORIENTED_EDGE('',*,*,#7426,.F.);
#10628=ORIENTED_EDGE('',*,*,#7524,.F.);
#10629=ORIENTED_EDGE('',*,*,#7422,.F.);
#10630=ORIENTED_EDGE('',*,*,#7522,.F.);
#10631=ORIENTED_EDGE('',*,*,#7423,.F.);
#10632=ORIENTED_EDGE('',*,*,#7416,.F.);
#10633=ORIENTED_EDGE('',*,*,#7523,.F.);
#10634=ORIENTED_EDGE('',*,*,#7418,.F.);
#10635=ORIENTED_EDGE('',*,*,#7521,.T.);
#10636=ORIENTED_EDGE('',*,*,#7420,.T.);
#10637=ORIENTED_EDGE('',*,*,#7524,.T.);
#10638=ORIENTED_EDGE('',*,*,#7425,.T.);
#10639=ORIENTED_EDGE('',*,*,#7407,.F.);
#10640=ORIENTED_EDGE('',*,*,#7427,.T.);
#10641=ORIENTED_EDGE('',*,*,#7405,.T.);
#10642=ORIENTED_EDGE('',*,*,#7428,.F.);
#10643=ORIENTED_EDGE('',*,*,#7386,.F.);
#10644=ORIENTED_EDGE('',*,*,#7525,.F.);
#10645=ORIENTED_EDGE('',*,*,#7414,.F.);
#10646=ORIENTED_EDGE('',*,*,#7526,.F.);
#10647=ORIENTED_EDGE('',*,*,#7527,.T.);
#10648=ORIENTED_EDGE('',*,*,#7384,.T.);
#10649=ORIENTED_EDGE('',*,*,#7528,.T.);
#10650=ORIENTED_EDGE('',*,*,#7412,.T.);
#10651=ORIENTED_EDGE('',*,*,#7387,.F.);
#10652=ORIENTED_EDGE('',*,*,#7526,.T.);
#10653=ORIENTED_EDGE('',*,*,#7413,.F.);
#10654=ORIENTED_EDGE('',*,*,#7528,.F.);
#10655=ORIENTED_EDGE('',*,*,#7385,.F.);
#10656=ORIENTED_EDGE('',*,*,#7527,.F.);
#10657=ORIENTED_EDGE('',*,*,#7415,.F.);
#10658=ORIENTED_EDGE('',*,*,#7525,.T.);
#10659=ORIENTED_EDGE('',*,*,#7397,.F.);
#10660=ORIENTED_EDGE('',*,*,#7529,.F.);
#10661=ORIENTED_EDGE('',*,*,#7400,.F.);
#10662=ORIENTED_EDGE('',*,*,#7530,.T.);
#10663=ORIENTED_EDGE('',*,*,#7395,.F.);
#10664=ORIENTED_EDGE('',*,*,#7531,.T.);
#10665=ORIENTED_EDGE('',*,*,#7402,.F.);
#10666=ORIENTED_EDGE('',*,*,#7532,.F.);
#10667=ORIENTED_EDGE('',*,*,#7398,.F.);
#10668=ORIENTED_EDGE('',*,*,#7530,.F.);
#10669=ORIENTED_EDGE('',*,*,#7399,.F.);
#10670=ORIENTED_EDGE('',*,*,#7392,.F.);
#10671=ORIENTED_EDGE('',*,*,#7531,.F.);
#10672=ORIENTED_EDGE('',*,*,#7394,.F.);
#10673=ORIENTED_EDGE('',*,*,#7529,.T.);
#10674=ORIENTED_EDGE('',*,*,#7396,.T.);
#10675=ORIENTED_EDGE('',*,*,#7532,.T.);
#10676=ORIENTED_EDGE('',*,*,#7401,.T.);
#10677=ORIENTED_EDGE('',*,*,#7383,.F.);
#10678=ORIENTED_EDGE('',*,*,#7403,.T.);
#10679=ORIENTED_EDGE('',*,*,#7381,.T.);
#10680=ORIENTED_EDGE('',*,*,#7404,.F.);
#10681=ORIENTED_EDGE('',*,*,#7362,.F.);
#10682=ORIENTED_EDGE('',*,*,#7533,.F.);
#10683=ORIENTED_EDGE('',*,*,#7390,.F.);
#10684=ORIENTED_EDGE('',*,*,#7534,.F.);
#10685=ORIENTED_EDGE('',*,*,#7535,.T.);
#10686=ORIENTED_EDGE('',*,*,#7360,.T.);
#10687=ORIENTED_EDGE('',*,*,#7536,.T.);
#10688=ORIENTED_EDGE('',*,*,#7388,.T.);
#10689=ORIENTED_EDGE('',*,*,#7363,.F.);
#10690=ORIENTED_EDGE('',*,*,#7534,.T.);
#10691=ORIENTED_EDGE('',*,*,#7389,.F.);
#10692=ORIENTED_EDGE('',*,*,#7536,.F.);
#10693=ORIENTED_EDGE('',*,*,#7361,.F.);
#10694=ORIENTED_EDGE('',*,*,#7535,.F.);
#10695=ORIENTED_EDGE('',*,*,#7391,.F.);
#10696=ORIENTED_EDGE('',*,*,#7533,.T.);
#10697=ORIENTED_EDGE('',*,*,#7373,.F.);
#10698=ORIENTED_EDGE('',*,*,#7537,.F.);
#10699=ORIENTED_EDGE('',*,*,#7376,.F.);
#10700=ORIENTED_EDGE('',*,*,#7538,.T.);
#10701=ORIENTED_EDGE('',*,*,#7371,.F.);
#10702=ORIENTED_EDGE('',*,*,#7539,.T.);
#10703=ORIENTED_EDGE('',*,*,#7378,.F.);
#10704=ORIENTED_EDGE('',*,*,#7540,.F.);
#10705=ORIENTED_EDGE('',*,*,#7374,.F.);
#10706=ORIENTED_EDGE('',*,*,#7538,.F.);
#10707=ORIENTED_EDGE('',*,*,#7375,.F.);
#10708=ORIENTED_EDGE('',*,*,#7368,.F.);
#10709=ORIENTED_EDGE('',*,*,#7539,.F.);
#10710=ORIENTED_EDGE('',*,*,#7370,.F.);
#10711=ORIENTED_EDGE('',*,*,#7537,.T.);
#10712=ORIENTED_EDGE('',*,*,#7372,.T.);
#10713=ORIENTED_EDGE('',*,*,#7540,.T.);
#10714=ORIENTED_EDGE('',*,*,#7377,.T.);
#10715=ORIENTED_EDGE('',*,*,#7359,.F.);
#10716=ORIENTED_EDGE('',*,*,#7379,.T.);
#10717=ORIENTED_EDGE('',*,*,#7357,.T.);
#10718=ORIENTED_EDGE('',*,*,#7380,.F.);
#10719=ORIENTED_EDGE('',*,*,#7338,.F.);
#10720=ORIENTED_EDGE('',*,*,#7541,.F.);
#10721=ORIENTED_EDGE('',*,*,#7366,.F.);
#10722=ORIENTED_EDGE('',*,*,#7542,.F.);
#10723=ORIENTED_EDGE('',*,*,#7543,.T.);
#10724=ORIENTED_EDGE('',*,*,#7336,.T.);
#10725=ORIENTED_EDGE('',*,*,#7544,.T.);
#10726=ORIENTED_EDGE('',*,*,#7364,.T.);
#10727=ORIENTED_EDGE('',*,*,#7339,.F.);
#10728=ORIENTED_EDGE('',*,*,#7542,.T.);
#10729=ORIENTED_EDGE('',*,*,#7365,.F.);
#10730=ORIENTED_EDGE('',*,*,#7544,.F.);
#10731=ORIENTED_EDGE('',*,*,#7337,.F.);
#10732=ORIENTED_EDGE('',*,*,#7543,.F.);
#10733=ORIENTED_EDGE('',*,*,#7367,.F.);
#10734=ORIENTED_EDGE('',*,*,#7541,.T.);
#10735=ORIENTED_EDGE('',*,*,#7349,.F.);
#10736=ORIENTED_EDGE('',*,*,#7545,.F.);
#10737=ORIENTED_EDGE('',*,*,#7352,.F.);
#10738=ORIENTED_EDGE('',*,*,#7546,.T.);
#10739=ORIENTED_EDGE('',*,*,#7347,.F.);
#10740=ORIENTED_EDGE('',*,*,#7547,.T.);
#10741=ORIENTED_EDGE('',*,*,#7354,.F.);
#10742=ORIENTED_EDGE('',*,*,#7548,.F.);
#10743=ORIENTED_EDGE('',*,*,#7350,.F.);
#10744=ORIENTED_EDGE('',*,*,#7546,.F.);
#10745=ORIENTED_EDGE('',*,*,#7351,.F.);
#10746=ORIENTED_EDGE('',*,*,#7344,.F.);
#10747=ORIENTED_EDGE('',*,*,#7547,.F.);
#10748=ORIENTED_EDGE('',*,*,#7346,.F.);
#10749=ORIENTED_EDGE('',*,*,#7545,.T.);
#10750=ORIENTED_EDGE('',*,*,#7348,.T.);
#10751=ORIENTED_EDGE('',*,*,#7548,.T.);
#10752=ORIENTED_EDGE('',*,*,#7353,.T.);
#10753=ORIENTED_EDGE('',*,*,#7335,.F.);
#10754=ORIENTED_EDGE('',*,*,#7355,.T.);
#10755=ORIENTED_EDGE('',*,*,#7333,.T.);
#10756=ORIENTED_EDGE('',*,*,#7356,.F.);
#10757=ORIENTED_EDGE('',*,*,#7495,.F.);
#10758=ORIENTED_EDGE('',*,*,#7549,.F.);
#10759=ORIENTED_EDGE('',*,*,#7342,.F.);
#10760=ORIENTED_EDGE('',*,*,#7550,.F.);
#10761=ORIENTED_EDGE('',*,*,#7551,.T.);
#10762=ORIENTED_EDGE('',*,*,#7493,.T.);
#10763=ORIENTED_EDGE('',*,*,#7552,.T.);
#10764=ORIENTED_EDGE('',*,*,#7340,.T.);
#10765=ORIENTED_EDGE('',*,*,#7496,.F.);
#10766=ORIENTED_EDGE('',*,*,#7550,.T.);
#10767=ORIENTED_EDGE('',*,*,#7341,.F.);
#10768=ORIENTED_EDGE('',*,*,#7552,.F.);
#10769=ORIENTED_EDGE('',*,*,#7494,.F.);
#10770=ORIENTED_EDGE('',*,*,#7551,.F.);
#10771=ORIENTED_EDGE('',*,*,#7343,.F.);
#10772=ORIENTED_EDGE('',*,*,#7549,.T.);
#10773=ORIENTED_EDGE('',*,*,#7466,.F.);
#10774=ORIENTED_EDGE('',*,*,#7553,.T.);
#10775=ORIENTED_EDGE('',*,*,#7472,.T.);
#10776=ORIENTED_EDGE('',*,*,#7554,.T.);
#10777=ORIENTED_EDGE('',*,*,#7555,.F.);
#10778=ORIENTED_EDGE('',*,*,#7464,.T.);
#10779=ORIENTED_EDGE('',*,*,#7468,.T.);
#10780=ORIENTED_EDGE('',*,*,#7556,.F.);
#10781=ORIENTED_EDGE('',*,*,#7470,.F.);
#10782=ORIENTED_EDGE('',*,*,#7474,.F.);
#10783=ORIENTED_EDGE('',*,*,#7556,.T.);
#10784=ORIENTED_EDGE('',*,*,#7467,.T.);
#10785=ORIENTED_EDGE('',*,*,#7554,.F.);
#10786=ORIENTED_EDGE('',*,*,#7471,.F.);
#10787=ORIENTED_EDGE('',*,*,#7553,.F.);
#10788=ORIENTED_EDGE('',*,*,#7465,.T.);
#10789=ORIENTED_EDGE('',*,*,#7555,.T.);
#10790=ORIENTED_EDGE('',*,*,#7473,.F.);
#12181=CYLINDRICAL_SURFACE('',#13958,7.5);
#12182=CYLINDRICAL_SURFACE('',#13961,12.4653846153846);
#12183=CYLINDRICAL_SURFACE('',#13963,12.4653846153846);
#12184=CYLINDRICAL_SURFACE('',#13999,17.6897435897436);
#12185=CYLINDRICAL_SURFACE('',#14002,16.2686153846154);
#12186=CYLINDRICAL_SURFACE('',#14004,16.0346153846154);
#12187=CYLINDRICAL_SURFACE('',#14009,16.0346153846154);
#12188=CYLINDRICAL_SURFACE('',#14010,16.2686153846154);
#12189=CYLINDRICAL_SURFACE('',#14012,17.6897435897436);
#12190=CYLINDRICAL_SURFACE('',#14022,21.);
#12191=CYLINDRICAL_SURFACE('',#14127,14.25);
#12192=CYLINDRICAL_SURFACE('',#14130,15.1423076923077);
#12193=CYLINDRICAL_SURFACE('',#14143,15.1423076923077);
#12194=CYLINDRICAL_SURFACE('',#14144,14.25);
#12195=CYLINDRICAL_SURFACE('',#14153,15.1423076923077);
#12196=CYLINDRICAL_SURFACE('',#14154,14.25);
#12197=CYLINDRICAL_SURFACE('',#14155,14.25);
#12198=CYLINDRICAL_SURFACE('',#14158,15.1423076923077);
#12199=CYLINDRICAL_SURFACE('',#14171,15.1423076923077);
#12200=CYLINDRICAL_SURFACE('',#14172,14.25);
#12201=CYLINDRICAL_SURFACE('',#14173,14.25);
#12202=CYLINDRICAL_SURFACE('',#14176,15.1423076923077);
#12203=CYLINDRICAL_SURFACE('',#14189,15.1423076923077);
#12204=CYLINDRICAL_SURFACE('',#14190,14.25);
#12205=CYLINDRICAL_SURFACE('',#14191,14.25);
#12206=CYLINDRICAL_SURFACE('',#14194,15.1423076923077);
#12207=CYLINDRICAL_SURFACE('',#14207,15.1423076923077);
#12208=CYLINDRICAL_SURFACE('',#14208,14.25);
#12209=CYLINDRICAL_SURFACE('',#14209,14.25);
#12210=CYLINDRICAL_SURFACE('',#14212,15.1423076923077);
#12211=CYLINDRICAL_SURFACE('',#14225,15.1423076923077);
#12212=CYLINDRICAL_SURFACE('',#14226,14.25);
#12213=CYLINDRICAL_SURFACE('',#14227,14.25);
#12214=CYLINDRICAL_SURFACE('',#14230,15.1423076923077);
#12215=CYLINDRICAL_SURFACE('',#14243,15.1423076923077);
#12216=CYLINDRICAL_SURFACE('',#14244,14.25);
#12217=CYLINDRICAL_SURFACE('',#14251,15.1423076923077);
#12218=CYLINDRICAL_SURFACE('',#14252,14.25);
#12672=ADVANCED_FACE('',(#1660),#130,.F.);
#12673=ADVANCED_FACE('',(#1661),#131,.T.);
#12674=ADVANCED_FACE('',(#1662),#132,.T.);
#12675=ADVANCED_FACE('',(#1663),#103,.F.);
#12676=ADVANCED_FACE('',(#1664),#12181,.F.);
#12677=ADVANCED_FACE('',(#1665),#104,.F.);
#12678=ADVANCED_FACE('',(#1666),#12182,.T.);
#12679=ADVANCED_FACE('',(#1667),#12183,.T.);
#12680=ADVANCED_FACE('',(#1668,#333),#1125,.F.);
#12681=ADVANCED_FACE('',(#1669,#334),#1126,.F.);
#12682=ADVANCED_FACE('',(#1670),#57,.T.);
#12683=ADVANCED_FACE('',(#1671),#58,.T.);
#12684=ADVANCED_FACE('',(#1672),#59,.T.);
#12685=ADVANCED_FACE('',(#1673),#60,.T.);
#12686=ADVANCED_FACE('',(#1674),#61,.T.);
#12687=ADVANCED_FACE('',(#1675),#62,.T.);
#12688=ADVANCED_FACE('',(#1676),#63,.T.);
#12689=ADVANCED_FACE('',(#1677),#133,.T.);
#12690=ADVANCED_FACE('',(#1678),#134,.T.);
#12691=ADVANCED_FACE('',(#1679),#135,.T.);
#12692=ADVANCED_FACE('',(#1680),#136,.T.);
#12693=ADVANCED_FACE('',(#1681),#12184,.F.);
#12694=ADVANCED_FACE('',(#1682),#12185,.F.);
#12695=ADVANCED_FACE('',(#1683),#12186,.F.);
#12696=ADVANCED_FACE('',(#1684),#137,.F.);
#12697=ADVANCED_FACE('',(#1685),#12187,.F.);
#12698=ADVANCED_FACE('',(#1686),#12188,.F.);
#12699=ADVANCED_FACE('',(#1687),#12189,.F.);
#12700=ADVANCED_FACE('',(#1688),#105,.T.);
#12701=ADVANCED_FACE('',(#1689),#106,.T.);
#12702=ADVANCED_FACE('',(#1690),#12190,.T.);
#12703=ADVANCED_FACE('',(#1691,#335),#1127,.F.);
#12704=ADVANCED_FACE('',(#1692,#336),#1128,.F.);
#12705=ADVANCED_FACE('',(#1693,#337),#1129,.T.);
#12706=ADVANCED_FACE('',(#1694,#338),#1130,.T.);
#12707=ADVANCED_FACE('',(#1695,#339),#1131,.T.);
#12708=ADVANCED_FACE('',(#1696,#340),#1132,.T.);
#12709=ADVANCED_FACE('',(#1697,#341,#342),#138,.T.);
#12710=ADVANCED_FACE('',(#1698,#343,#344),#64,.F.);
#12711=ADVANCED_FACE('',(#1699,#345,#346),#139,.T.);
#12712=ADVANCED_FACE('',(#1700,#347,#348),#65,.F.);
#12713=ADVANCED_FACE('',(#1701,#349,#350),#140,.T.);
#12714=ADVANCED_FACE('',(#1702,#351,#352),#66,.F.);
#12715=ADVANCED_FACE('',(#1703,#353,#354),#141,.T.);
#12716=ADVANCED_FACE('',(#1704,#355,#356),#67,.F.);
#12717=ADVANCED_FACE('',(#1705,#357,#358),#142,.T.);
#12718=ADVANCED_FACE('',(#1706,#359,#360),#68,.F.);
#12719=ADVANCED_FACE('',(#1707,#361,#362),#143,.T.);
#12720=ADVANCED_FACE('',(#1708,#363,#364),#69,.F.);
#12721=ADVANCED_FACE('',(#1709,#365,#366),#70,.F.);
#12722=ADVANCED_FACE('',(#1710,#367,#368),#144,.T.);
#12723=ADVANCED_FACE('',(#1711),#12191,.F.);
#12724=ADVANCED_FACE('',(#1712),#12192,.T.);
#12725=ADVANCED_FACE('',(#1713),#1133,.T.);
#12726=ADVANCED_FACE('',(#1714),#1134,.F.);
#12727=ADVANCED_FACE('',(#1715,#369),#1135,.T.);
#12728=ADVANCED_FACE('',(#1716,#370),#1136,.T.);
#12729=ADVANCED_FACE('',(#1717),#1137,.T.);
#12730=ADVANCED_FACE('',(#1718),#1138,.F.);
#12731=ADVANCED_FACE('',(#1719),#12193,.T.);
#12732=ADVANCED_FACE('',(#1720),#12194,.F.);
#12733=ADVANCED_FACE('',(#1721,#371),#1139,.T.);
#12734=ADVANCED_FACE('',(#1722,#372),#1140,.T.);
#12735=ADVANCED_FACE('',(#1723),#1141,.F.);
#12736=ADVANCED_FACE('',(#1724),#1142,.T.);
#12737=ADVANCED_FACE('',(#1725),#12195,.T.);
#12738=ADVANCED_FACE('',(#1726),#12196,.F.);
#12739=ADVANCED_FACE('',(#1727),#12197,.F.);
#12740=ADVANCED_FACE('',(#1728),#12198,.T.);
#12741=ADVANCED_FACE('',(#1729),#1143,.F.);
#12742=ADVANCED_FACE('',(#1730),#1144,.T.);
#12743=ADVANCED_FACE('',(#1731,#373),#1145,.T.);
#12744=ADVANCED_FACE('',(#1732,#374),#1146,.T.);
#12745=ADVANCED_FACE('',(#1733),#1147,.F.);
#12746=ADVANCED_FACE('',(#1734),#1148,.T.);
#12747=ADVANCED_FACE('',(#1735),#12199,.T.);
#12748=ADVANCED_FACE('',(#1736),#12200,.F.);
#12749=ADVANCED_FACE('',(#1737),#12201,.F.);
#12750=ADVANCED_FACE('',(#1738),#12202,.T.);
#12751=ADVANCED_FACE('',(#1739),#1149,.F.);
#12752=ADVANCED_FACE('',(#1740),#1150,.T.);
#12753=ADVANCED_FACE('',(#1741,#375),#1151,.T.);
#12754=ADVANCED_FACE('',(#1742,#376),#1152,.T.);
#12755=ADVANCED_FACE('',(#1743),#1153,.F.);
#12756=ADVANCED_FACE('',(#1744),#1154,.T.);
#12757=ADVANCED_FACE('',(#1745),#12203,.T.);
#12758=ADVANCED_FACE('',(#1746),#12204,.F.);
#12759=ADVANCED_FACE('',(#1747),#12205,.F.);
#12760=ADVANCED_FACE('',(#1748),#12206,.T.);
#12761=ADVANCED_FACE('',(#1749),#1155,.F.);
#12762=ADVANCED_FACE('',(#1750),#1156,.T.);
#12763=ADVANCED_FACE('',(#1751,#377),#1157,.T.);
#12764=ADVANCED_FACE('',(#1752,#378),#1158,.T.);
#12765=ADVANCED_FACE('',(#1753),#1159,.F.);
#12766=ADVANCED_FACE('',(#1754),#1160,.T.);
#12767=ADVANCED_FACE('',(#1755),#12207,.T.);
#12768=ADVANCED_FACE('',(#1756),#12208,.F.);
#12769=ADVANCED_FACE('',(#1757),#12209,.F.);
#12770=ADVANCED_FACE('',(#1758),#12210,.T.);
#12771=ADVANCED_FACE('',(#1759),#1161,.F.);
#12772=ADVANCED_FACE('',(#1760),#1162,.T.);
#12773=ADVANCED_FACE('',(#1761,#379),#1163,.T.);
#12774=ADVANCED_FACE('',(#1762,#380),#1164,.T.);
#12775=ADVANCED_FACE('',(#1763),#1165,.F.);
#12776=ADVANCED_FACE('',(#1764),#1166,.T.);
#12777=ADVANCED_FACE('',(#1765),#12211,.T.);
#12778=ADVANCED_FACE('',(#1766),#12212,.F.);
#12779=ADVANCED_FACE('',(#1767),#12213,.F.);
#12780=ADVANCED_FACE('',(#1768),#12214,.T.);
#12781=ADVANCED_FACE('',(#1769),#1167,.F.);
#12782=ADVANCED_FACE('',(#1770),#1168,.T.);
#12783=ADVANCED_FACE('',(#1771,#381),#1169,.T.);
#12784=ADVANCED_FACE('',(#1772,#382),#1170,.T.);
#12785=ADVANCED_FACE('',(#1773),#1171,.F.);
#12786=ADVANCED_FACE('',(#1774),#1172,.T.);
#12787=ADVANCED_FACE('',(#1775),#12215,.T.);
#12788=ADVANCED_FACE('',(#1776),#12216,.F.);
#12789=ADVANCED_FACE('',(#1777),#1173,.T.);
#12790=ADVANCED_FACE('',(#1778),#1174,.F.);
#12791=ADVANCED_FACE('',(#1779),#12217,.T.);
#12792=ADVANCED_FACE('',(#1780),#12218,.F.);
#13063=CLOSED_SHELL('',(#12672,#12673,#12674,#12675,#12676,#12677,#12678,
#12679,#12680,#12681));
#13064=CLOSED_SHELL('',(#12682));
#13065=CLOSED_SHELL('',(#12683));
#13066=CLOSED_SHELL('',(#12684));
#13067=CLOSED_SHELL('',(#12685));
#13068=CLOSED_SHELL('',(#12686));
#13069=CLOSED_SHELL('',(#12687));
#13070=CLOSED_SHELL('',(#12688));
#13071=CLOSED_SHELL('',(#12689,#12690,#12691,#12692,#12693,#12694,#12695,
#12696,#12697,#12698,#12699,#12700,#12701,#12702,#12703,#12704,#12705,#12706,
#12707,#12708));
#13072=CLOSED_SHELL('',(#12709,#12710,#12711,#12712,#12713,#12714,#12715,
#12716,#12717,#12718,#12719,#12720,#12721,#12722,#12723,#12724,#12725,#12726,
#12727,#12728,#12729,#12730,#12731,#12732,#12733,#12734,#12735,#12736,#12737,
#12738,#12739,#12740,#12741,#12742,#12743,#12744,#12745,#12746,#12747,#12748,
#12749,#12750,#12751,#12752,#12753,#12754,#12755,#12756,#12757,#12758,#12759,
#12760,#12761,#12762,#12763,#12764,#12765,#12766,#12767,#12768,#12769,#12770,
#12771,#12772,#12773,#12774,#12775,#12776,#12777,#12778,#12779,#12780,#12781,
#12782,#12783,#12784,#12785,#12786,#12787,#12788,#12789,#12790,#12791,#12792));
#13940=AXIS2_PLACEMENT_3D('',#39437,#16803,#16804);
#13941=AXIS2_PLACEMENT_3D('',#39438,#16805,#16806);
#13942=AXIS2_PLACEMENT_3D('',#39440,#16807,#16808);
#13943=AXIS2_PLACEMENT_3D('',#39442,#16809,#16810);
#13944=AXIS2_PLACEMENT_3D('',#39443,#16811,#16812);
#13945=AXIS2_PLACEMENT_3D('',#39444,#16813,#16814);
#13946=AXIS2_PLACEMENT_3D('',#39447,#16815,#16816);
#13947=AXIS2_PLACEMENT_3D('',#39448,#16817,#16818);
#13948=AXIS2_PLACEMENT_3D('',#39450,#16819,#16820);
#13949=AXIS2_PLACEMENT_3D('',#39452,#16821,#16822);
#13950=AXIS2_PLACEMENT_3D('',#39453,#16823,#16824);
#13951=AXIS2_PLACEMENT_3D('',#39454,#16825,#16826);
#13952=AXIS2_PLACEMENT_3D('',#39457,#16827,#16828);
#13953=AXIS2_PLACEMENT_3D('',#39458,#16829,#16830);
#13954=AXIS2_PLACEMENT_3D('',#39460,#16831,#16832);
#13955=AXIS2_PLACEMENT_3D('',#39461,#16833,#16834);
#13956=AXIS2_PLACEMENT_3D('',#39462,#16835,#16836);
#13957=AXIS2_PLACEMENT_3D('',#39465,#16838,#16839);
#13958=AXIS2_PLACEMENT_3D('',#39466,#16840,#16841);
#13959=AXIS2_PLACEMENT_3D('',#39468,#16843,#16844);
#13960=AXIS2_PLACEMENT_3D('',#39471,#16846,#16847);
#13961=AXIS2_PLACEMENT_3D('',#39472,#16848,#16849);
#13962=AXIS2_PLACEMENT_3D('',#39475,#16851,#16852);
#13963=AXIS2_PLACEMENT_3D('',#39476,#16853,#16854);
#13964=AXIS2_PLACEMENT_3D('',#39478,#16855,#16856);
#13965=AXIS2_PLACEMENT_3D('',#39480,#16858,#16859);
#13966=AXIS2_PLACEMENT_3D('',#39481,#16860,#16861);
#13967=AXIS2_PLACEMENT_3D('',#39482,#16862,#16863);
#13968=AXIS2_PLACEMENT_3D('',#39485,#16864,#16865);
#13969=AXIS2_PLACEMENT_3D('',#39486,#16866,#16867);
#13970=AXIS2_PLACEMENT_3D('',#39489,#16868,#16869);
#13971=AXIS2_PLACEMENT_3D('',#39490,#16870,#16871);
#13972=AXIS2_PLACEMENT_3D('',#39493,#16872,#16873);
#13973=AXIS2_PLACEMENT_3D('',#39494,#16874,#16875);
#13974=AXIS2_PLACEMENT_3D('',#39497,#16876,#16877);
#13975=AXIS2_PLACEMENT_3D('',#39498,#16878,#16879);
#13976=AXIS2_PLACEMENT_3D('',#39501,#16880,#16881);
#13977=AXIS2_PLACEMENT_3D('',#39502,#16882,#16883);
#13978=AXIS2_PLACEMENT_3D('',#39505,#16884,#16885);
#13979=AXIS2_PLACEMENT_3D('',#39506,#16886,#16887);
#13980=AXIS2_PLACEMENT_3D('',#39509,#16888,#16889);
#13981=AXIS2_PLACEMENT_3D('',#39510,#16890,#16891);
#13982=AXIS2_PLACEMENT_3D('',#39512,#16892,#16893);
#13983=AXIS2_PLACEMENT_3D('',#39514,#16894,#16895);
#13984=AXIS2_PLACEMENT_3D('',#39516,#16896,#16897);
#13985=AXIS2_PLACEMENT_3D('',#39517,#16898,#16899);
#13986=AXIS2_PLACEMENT_3D('',#39518,#16900,#16901);
#13987=AXIS2_PLACEMENT_3D('',#39520,#16902,#16903);
#13988=AXIS2_PLACEMENT_3D('',#39522,#16904,#16905);
#13989=AXIS2_PLACEMENT_3D('',#39523,#16906,#16907);
#13990=AXIS2_PLACEMENT_3D('',#39524,#16908,#16909);
#13991=AXIS2_PLACEMENT_3D('',#39526,#16910,#16911);
#13992=AXIS2_PLACEMENT_3D('',#39528,#16912,#16913);
#13993=AXIS2_PLACEMENT_3D('',#39529,#16914,#16915);
#13994=AXIS2_PLACEMENT_3D('',#39530,#16916,#16917);
#13995=AXIS2_PLACEMENT_3D('',#39533,#16918,#16919);
#13996=AXIS2_PLACEMENT_3D('',#39534,#16920,#16921);
#13997=AXIS2_PLACEMENT_3D('',#39536,#16922,#16923);
#13998=AXIS2_PLACEMENT_3D('',#39537,#16924,#16925);
#13999=AXIS2_PLACEMENT_3D('',#39538,#16926,#16927);
#14000=AXIS2_PLACEMENT_3D('',#39540,#16928,#16929);
#14001=AXIS2_PLACEMENT_3D('',#39543,#16931,#16932);
#14002=AXIS2_PLACEMENT_3D('',#39544,#16933,#16934);
#14003=AXIS2_PLACEMENT_3D('',#39546,#16935,#16936);
#14004=AXIS2_PLACEMENT_3D('',#39548,#16938,#16939);
#14005=AXIS2_PLACEMENT_3D('',#39551,#16941,#16942);
#14006=AXIS2_PLACEMENT_3D('',#39552,#16943,#16944);
#14007=AXIS2_PLACEMENT_3D('',#39554,#16945,#16946);
#14008=AXIS2_PLACEMENT_3D('',#39555,#16947,#16948);
#14009=AXIS2_PLACEMENT_3D('',#39556,#16949,#16950);
#14010=AXIS2_PLACEMENT_3D('',#39558,#16952,#16953);
#14011=AXIS2_PLACEMENT_3D('',#39561,#16955,#16956);
#14012=AXIS2_PLACEMENT_3D('',#39562,#16957,#16958);
#14013=AXIS2_PLACEMENT_3D('',#39564,#16959,#16960);
#14014=AXIS2_PLACEMENT_3D('',#39567,#16962,#16963);
#14015=AXIS2_PLACEMENT_3D('',#39568,#16964,#16965);
#14016=AXIS2_PLACEMENT_3D('',#39570,#16966,#16967);
#14017=AXIS2_PLACEMENT_3D('',#39573,#16969,#16970);
#14018=AXIS2_PLACEMENT_3D('',#39574,#16971,#16972);
#14019=AXIS2_PLACEMENT_3D('',#39577,#16973,#16974);
#14020=AXIS2_PLACEMENT_3D('',#39580,#16976,#16977);
#14021=AXIS2_PLACEMENT_3D('',#39581,#16978,#16979);
#14022=AXIS2_PLACEMENT_3D('',#39582,#16980,#16981);
#14023=AXIS2_PLACEMENT_3D('',#39584,#16983,#16984);
#14024=AXIS2_PLACEMENT_3D('',#39585,#16985,#16986);
#14025=AXIS2_PLACEMENT_3D('',#39586,#16987,#16988);
#14026=AXIS2_PLACEMENT_3D('',#39587,#16989,#16990);
#14027=AXIS2_PLACEMENT_3D('',#39588,#16991,#16992);
#14028=AXIS2_PLACEMENT_3D('',#39589,#16993,#16994);
#14029=AXIS2_PLACEMENT_3D('',#39590,#16995,#16996);
#14030=AXIS2_PLACEMENT_3D('',#39592,#16997,#16998);
#14031=AXIS2_PLACEMENT_3D('',#39594,#16999,#17000);
#14032=AXIS2_PLACEMENT_3D('',#39595,#17001,#17002);
#14033=AXIS2_PLACEMENT_3D('',#39704,#17003,#17004);
#14034=AXIS2_PLACEMENT_3D('',#39707,#17005,#17006);
#14035=AXIS2_PLACEMENT_3D('',#39709,#17007,#17008);
#14036=AXIS2_PLACEMENT_3D('',#39711,#17009,#17010);
#14037=AXIS2_PLACEMENT_3D('',#39721,#17011,#17012);
#14038=AXIS2_PLACEMENT_3D('',#39730,#17013,#17014);
#14039=AXIS2_PLACEMENT_3D('',#39732,#17015,#17016);
#14040=AXIS2_PLACEMENT_3D('',#39741,#17017,#17018);
#14041=AXIS2_PLACEMENT_3D('',#39749,#17019,#17020);
#14042=AXIS2_PLACEMENT_3D('',#39751,#17021,#17022);
#14043=AXIS2_PLACEMENT_3D('',#39752,#17023,#17024);
#14044=AXIS2_PLACEMENT_3D('',#39754,#17025,#17026);
#14045=AXIS2_PLACEMENT_3D('',#39756,#17027,#17028);
#14046=AXIS2_PLACEMENT_3D('',#39757,#17029,#17030);
#14047=AXIS2_PLACEMENT_3D('',#39866,#17031,#17032);
#14048=AXIS2_PLACEMENT_3D('',#39869,#17033,#17034);
#14049=AXIS2_PLACEMENT_3D('',#39871,#17035,#17036);
#14050=AXIS2_PLACEMENT_3D('',#39873,#17037,#17038);
#14051=AXIS2_PLACEMENT_3D('',#39883,#17039,#17040);
#14052=AXIS2_PLACEMENT_3D('',#39892,#17041,#17042);
#14053=AXIS2_PLACEMENT_3D('',#39894,#17043,#17044);
#14054=AXIS2_PLACEMENT_3D('',#39903,#17045,#17046);
#14055=AXIS2_PLACEMENT_3D('',#39911,#17047,#17048);
#14056=AXIS2_PLACEMENT_3D('',#39913,#17049,#17050);
#14057=AXIS2_PLACEMENT_3D('',#39914,#17051,#17052);
#14058=AXIS2_PLACEMENT_3D('',#39916,#17053,#17054);
#14059=AXIS2_PLACEMENT_3D('',#39918,#17055,#17056);
#14060=AXIS2_PLACEMENT_3D('',#39919,#17057,#17058);
#14061=AXIS2_PLACEMENT_3D('',#40028,#17059,#17060);
#14062=AXIS2_PLACEMENT_3D('',#40031,#17061,#17062);
#14063=AXIS2_PLACEMENT_3D('',#40033,#17063,#17064);
#14064=AXIS2_PLACEMENT_3D('',#40035,#17065,#17066);
#14065=AXIS2_PLACEMENT_3D('',#40045,#17067,#17068);
#14066=AXIS2_PLACEMENT_3D('',#40054,#17069,#17070);
#14067=AXIS2_PLACEMENT_3D('',#40056,#17071,#17072);
#14068=AXIS2_PLACEMENT_3D('',#40065,#17073,#17074);
#14069=AXIS2_PLACEMENT_3D('',#40073,#17075,#17076);
#14070=AXIS2_PLACEMENT_3D('',#40075,#17077,#17078);
#14071=AXIS2_PLACEMENT_3D('',#40076,#17079,#17080);
#14072=AXIS2_PLACEMENT_3D('',#40078,#17081,#17082);
#14073=AXIS2_PLACEMENT_3D('',#40080,#17083,#17084);
#14074=AXIS2_PLACEMENT_3D('',#40081,#17085,#17086);
#14075=AXIS2_PLACEMENT_3D('',#40190,#17087,#17088);
#14076=AXIS2_PLACEMENT_3D('',#40193,#17089,#17090);
#14077=AXIS2_PLACEMENT_3D('',#40195,#17091,#17092);
#14078=AXIS2_PLACEMENT_3D('',#40197,#17093,#17094);
#14079=AXIS2_PLACEMENT_3D('',#40207,#17095,#17096);
#14080=AXIS2_PLACEMENT_3D('',#40216,#17097,#17098);
#14081=AXIS2_PLACEMENT_3D('',#40218,#17099,#17100);
#14082=AXIS2_PLACEMENT_3D('',#40227,#17101,#17102);
#14083=AXIS2_PLACEMENT_3D('',#40235,#17103,#17104);
#14084=AXIS2_PLACEMENT_3D('',#40237,#17105,#17106);
#14085=AXIS2_PLACEMENT_3D('',#40238,#17107,#17108);
#14086=AXIS2_PLACEMENT_3D('',#40240,#17109,#17110);
#14087=AXIS2_PLACEMENT_3D('',#40242,#17111,#17112);
#14088=AXIS2_PLACEMENT_3D('',#40243,#17113,#17114);
#14089=AXIS2_PLACEMENT_3D('',#40352,#17115,#17116);
#14090=AXIS2_PLACEMENT_3D('',#40355,#17117,#17118);
#14091=AXIS2_PLACEMENT_3D('',#40357,#17119,#17120);
#14092=AXIS2_PLACEMENT_3D('',#40359,#17121,#17122);
#14093=AXIS2_PLACEMENT_3D('',#40369,#17123,#17124);
#14094=AXIS2_PLACEMENT_3D('',#40378,#17125,#17126);
#14095=AXIS2_PLACEMENT_3D('',#40380,#17127,#17128);
#14096=AXIS2_PLACEMENT_3D('',#40389,#17129,#17130);
#14097=AXIS2_PLACEMENT_3D('',#40397,#17131,#17132);
#14098=AXIS2_PLACEMENT_3D('',#40399,#17133,#17134);
#14099=AXIS2_PLACEMENT_3D('',#40400,#17135,#17136);
#14100=AXIS2_PLACEMENT_3D('',#40402,#17137,#17138);
#14101=AXIS2_PLACEMENT_3D('',#40404,#17139,#17140);
#14102=AXIS2_PLACEMENT_3D('',#40405,#17141,#17142);
#14103=AXIS2_PLACEMENT_3D('',#40514,#17143,#17144);
#14104=AXIS2_PLACEMENT_3D('',#40517,#17145,#17146);
#14105=AXIS2_PLACEMENT_3D('',#40526,#17147,#17148);
#14106=AXIS2_PLACEMENT_3D('',#40534,#17149,#17150);
#14107=AXIS2_PLACEMENT_3D('',#40536,#17151,#17152);
#14108=AXIS2_PLACEMENT_3D('',#40538,#17153,#17154);
#14109=AXIS2_PLACEMENT_3D('',#40548,#17155,#17156);
#14110=AXIS2_PLACEMENT_3D('',#40557,#17157,#17158);
#14111=AXIS2_PLACEMENT_3D('',#40559,#17159,#17160);
#14112=AXIS2_PLACEMENT_3D('',#40561,#17161,#17162);
#14113=AXIS2_PLACEMENT_3D('',#40562,#17163,#17164);
#14114=AXIS2_PLACEMENT_3D('',#40565,#17165,#17166);
#14115=AXIS2_PLACEMENT_3D('',#40567,#17167,#17168);
#14116=AXIS2_PLACEMENT_3D('',#40569,#17169,#17170);
#14117=AXIS2_PLACEMENT_3D('',#40579,#17171,#17172);
#14118=AXIS2_PLACEMENT_3D('',#40588,#17173,#17174);
#14119=AXIS2_PLACEMENT_3D('',#40590,#17175,#17176);
#14120=AXIS2_PLACEMENT_3D('',#40599,#17177,#17178);
#14121=AXIS2_PLACEMENT_3D('',#40607,#17179,#17180);
#14122=AXIS2_PLACEMENT_3D('',#40609,#17181,#17182);
#14123=AXIS2_PLACEMENT_3D('',#40610,#17183,#17184);
#14124=AXIS2_PLACEMENT_3D('',#40612,#17185,#17186);
#14125=AXIS2_PLACEMENT_3D('',#40614,#17187,#17188);
#14126=AXIS2_PLACEMENT_3D('',#40615,#17189,#17190);
#14127=AXIS2_PLACEMENT_3D('',#40724,#17191,#17192);
#14128=AXIS2_PLACEMENT_3D('',#40725,#17193,#17194);
#14129=AXIS2_PLACEMENT_3D('',#40726,#17195,#17196);
#14130=AXIS2_PLACEMENT_3D('',#40727,#17197,#17198);
#14131=AXIS2_PLACEMENT_3D('',#40728,#17199,#17200);
#14132=AXIS2_PLACEMENT_3D('',#40729,#17201,#17202);
#14133=AXIS2_PLACEMENT_3D('',#40730,#17203,#17204);
#14134=AXIS2_PLACEMENT_3D('',#40731,#17205,#17206);
#14135=AXIS2_PLACEMENT_3D('',#40732,#17207,#17208);
#14136=AXIS2_PLACEMENT_3D('',#40733,#17209,#17210);
#14137=AXIS2_PLACEMENT_3D('',#40734,#17211,#17212);
#14138=AXIS2_PLACEMENT_3D('',#40735,#17213,#17214);
#14139=AXIS2_PLACEMENT_3D('',#40736,#17215,#17216);
#14140=AXIS2_PLACEMENT_3D('',#40737,#17217,#17218);
#14141=AXIS2_PLACEMENT_3D('',#40738,#17219,#17220);
#14142=AXIS2_PLACEMENT_3D('',#40739,#17221,#17222);
#14143=AXIS2_PLACEMENT_3D('',#40740,#17223,#17224);
#14144=AXIS2_PLACEMENT_3D('',#40741,#17225,#17226);
#14145=AXIS2_PLACEMENT_3D('',#40742,#17227,#17228);
#14146=AXIS2_PLACEMENT_3D('',#40743,#17229,#17230);
#14147=AXIS2_PLACEMENT_3D('',#40744,#17231,#17232);
#14148=AXIS2_PLACEMENT_3D('',#40745,#17233,#17234);
#14149=AXIS2_PLACEMENT_3D('',#40746,#17235,#17236);
#14150=AXIS2_PLACEMENT_3D('',#40747,#17237,#17238);
#14151=AXIS2_PLACEMENT_3D('',#40748,#17239,#17240);
#14152=AXIS2_PLACEMENT_3D('',#40749,#17241,#17242);
#14153=AXIS2_PLACEMENT_3D('',#40750,#17243,#17244);
#14154=AXIS2_PLACEMENT_3D('',#40751,#17245,#17246);
#14155=AXIS2_PLACEMENT_3D('',#40752,#17247,#17248);
#14156=AXIS2_PLACEMENT_3D('',#40753,#17249,#17250);
#14157=AXIS2_PLACEMENT_3D('',#40754,#17251,#17252);
#14158=AXIS2_PLACEMENT_3D('',#40755,#17253,#17254);
#14159=AXIS2_PLACEMENT_3D('',#40756,#17255,#17256);
#14160=AXIS2_PLACEMENT_3D('',#40757,#17257,#17258);
#14161=AXIS2_PLACEMENT_3D('',#40758,#17259,#17260);
#14162=AXIS2_PLACEMENT_3D('',#40759,#17261,#17262);
#14163=AXIS2_PLACEMENT_3D('',#40760,#17263,#17264);
#14164=AXIS2_PLACEMENT_3D('',#40761,#17265,#17266);
#14165=AXIS2_PLACEMENT_3D('',#40762,#17267,#17268);
#14166=AXIS2_PLACEMENT_3D('',#40763,#17269,#17270);
#14167=AXIS2_PLACEMENT_3D('',#40764,#17271,#17272);
#14168=AXIS2_PLACEMENT_3D('',#40765,#17273,#17274);
#14169=AXIS2_PLACEMENT_3D('',#40766,#17275,#17276);
#14170=AXIS2_PLACEMENT_3D('',#40767,#17277,#17278);
#14171=AXIS2_PLACEMENT_3D('',#40768,#17279,#17280);
#14172=AXIS2_PLACEMENT_3D('',#40769,#17281,#17282);
#14173=AXIS2_PLACEMENT_3D('',#40770,#17283,#17284);
#14174=AXIS2_PLACEMENT_3D('',#40771,#17285,#17286);
#14175=AXIS2_PLACEMENT_3D('',#40772,#17287,#17288);
#14176=AXIS2_PLACEMENT_3D('',#40773,#17289,#17290);
#14177=AXIS2_PLACEMENT_3D('',#40774,#17291,#17292);
#14178=AXIS2_PLACEMENT_3D('',#40775,#17293,#17294);
#14179=AXIS2_PLACEMENT_3D('',#40776,#17295,#17296);
#14180=AXIS2_PLACEMENT_3D('',#40777,#17297,#17298);
#14181=AXIS2_PLACEMENT_3D('',#40778,#17299,#17300);
#14182=AXIS2_PLACEMENT_3D('',#40779,#17301,#17302);
#14183=AXIS2_PLACEMENT_3D('',#40780,#17303,#17304);
#14184=AXIS2_PLACEMENT_3D('',#40781,#17305,#17306);
#14185=AXIS2_PLACEMENT_3D('',#40782,#17307,#17308);
#14186=AXIS2_PLACEMENT_3D('',#40783,#17309,#17310);
#14187=AXIS2_PLACEMENT_3D('',#40784,#17311,#17312);
#14188=AXIS2_PLACEMENT_3D('',#40785,#17313,#17314);
#14189=AXIS2_PLACEMENT_3D('',#40786,#17315,#17316);
#14190=AXIS2_PLACEMENT_3D('',#40787,#17317,#17318);
#14191=AXIS2_PLACEMENT_3D('',#40788,#17319,#17320);
#14192=AXIS2_PLACEMENT_3D('',#40789,#17321,#17322);
#14193=AXIS2_PLACEMENT_3D('',#40790,#17323,#17324);
#14194=AXIS2_PLACEMENT_3D('',#40791,#17325,#17326);
#14195=AXIS2_PLACEMENT_3D('',#40792,#17327,#17328);
#14196=AXIS2_PLACEMENT_3D('',#40793,#17329,#17330);
#14197=AXIS2_PLACEMENT_3D('',#40794,#17331,#17332);
#14198=AXIS2_PLACEMENT_3D('',#40795,#17333,#17334);
#14199=AXIS2_PLACEMENT_3D('',#40796,#17335,#17336);
#14200=AXIS2_PLACEMENT_3D('',#40797,#17337,#17338);
#14201=AXIS2_PLACEMENT_3D('',#40798,#17339,#17340);
#14202=AXIS2_PLACEMENT_3D('',#40799,#17341,#17342);
#14203=AXIS2_PLACEMENT_3D('',#40800,#17343,#17344);
#14204=AXIS2_PLACEMENT_3D('',#40801,#17345,#17346);
#14205=AXIS2_PLACEMENT_3D('',#40802,#17347,#17348);
#14206=AXIS2_PLACEMENT_3D('',#40803,#17349,#17350);
#14207=AXIS2_PLACEMENT_3D('',#40804,#17351,#17352);
#14208=AXIS2_PLACEMENT_3D('',#40805,#17353,#17354);
#14209=AXIS2_PLACEMENT_3D('',#40806,#17355,#17356);
#14210=AXIS2_PLACEMENT_3D('',#40807,#17357,#17358);
#14211=AXIS2_PLACEMENT_3D('',#40808,#17359,#17360);
#14212=AXIS2_PLACEMENT_3D('',#40809,#17361,#17362);
#14213=AXIS2_PLACEMENT_3D('',#40810,#17363,#17364);
#14214=AXIS2_PLACEMENT_3D('',#40811,#17365,#17366);
#14215=AXIS2_PLACEMENT_3D('',#40812,#17367,#17368);
#14216=AXIS2_PLACEMENT_3D('',#40813,#17369,#17370);
#14217=AXIS2_PLACEMENT_3D('',#40814,#17371,#17372);
#14218=AXIS2_PLACEMENT_3D('',#40815,#17373,#17374);
#14219=AXIS2_PLACEMENT_3D('',#40816,#17375,#17376);
#14220=AXIS2_PLACEMENT_3D('',#40817,#17377,#17378);
#14221=AXIS2_PLACEMENT_3D('',#40818,#17379,#17380);
#14222=AXIS2_PLACEMENT_3D('',#40819,#17381,#17382);
#14223=AXIS2_PLACEMENT_3D('',#40820,#17383,#17384);
#14224=AXIS2_PLACEMENT_3D('',#40821,#17385,#17386);
#14225=AXIS2_PLACEMENT_3D('',#40822,#17387,#17388);
#14226=AXIS2_PLACEMENT_3D('',#40823,#17389,#17390);
#14227=AXIS2_PLACEMENT_3D('',#40824,#17391,#17392);
#14228=AXIS2_PLACEMENT_3D('',#40825,#17393,#17394);
#14229=AXIS2_PLACEMENT_3D('',#40826,#17395,#17396);
#14230=AXIS2_PLACEMENT_3D('',#40827,#17397,#17398);
#14231=AXIS2_PLACEMENT_3D('',#40828,#17399,#17400);
#14232=AXIS2_PLACEMENT_3D('',#40829,#17401,#17402);
#14233=AXIS2_PLACEMENT_3D('',#40830,#17403,#17404);
#14234=AXIS2_PLACEMENT_3D('',#40831,#17405,#17406);
#14235=AXIS2_PLACEMENT_3D('',#40832,#17407,#17408);
#14236=AXIS2_PLACEMENT_3D('',#40833,#17409,#17410);
#14237=AXIS2_PLACEMENT_3D('',#40834,#17411,#17412);
#14238=AXIS2_PLACEMENT_3D('',#40835,#17413,#17414);
#14239=AXIS2_PLACEMENT_3D('',#40836,#17415,#17416);
#14240=AXIS2_PLACEMENT_3D('',#40837,#17417,#17418);
#14241=AXIS2_PLACEMENT_3D('',#40838,#17419,#17420);
#14242=AXIS2_PLACEMENT_3D('',#40839,#17421,#17422);
#14243=AXIS2_PLACEMENT_3D('',#40840,#17423,#17424);
#14244=AXIS2_PLACEMENT_3D('',#40841,#17425,#17426);
#14245=AXIS2_PLACEMENT_3D('',#40842,#17427,#17428);
#14246=AXIS2_PLACEMENT_3D('',#40843,#17429,#17430);
#14247=AXIS2_PLACEMENT_3D('',#40844,#17431,#17432);
#14248=AXIS2_PLACEMENT_3D('',#40845,#17433,#17434);
#14249=AXIS2_PLACEMENT_3D('',#40846,#17435,#17436);
#14250=AXIS2_PLACEMENT_3D('',#40847,#17437,#17438);
#14251=AXIS2_PLACEMENT_3D('',#40848,#17439,#17440);
#14252=AXIS2_PLACEMENT_3D('',#40849,#17441,#17442);
#16803=DIRECTION('axis',(0.,0.,1.));
#16804=DIRECTION('refdir',(1.,0.,0.));
#16805=DIRECTION('center_axis',(0.,-1.83697019872103E-16,1.));
#16806=DIRECTION('ref_axis',(0.,-1.,-1.83697019872103E-16));
#16807=DIRECTION('center_axis',(0.,-1.83697019872103E-16,1.));
#16808=DIRECTION('ref_axis',(0.,-1.,-1.83697019872103E-16));
#16809=DIRECTION('center_axis',(1.,1.22464679914735E-16,2.24963967399279E-32));
#16810=DIRECTION('ref_axis',(-1.22464679914735E-16,1.,1.83697019872103E-16));
#16811=DIRECTION('center_axis',(0.,-1.83697019872103E-16,1.));
#16812=DIRECTION('ref_axis',(0.,-1.,-1.83697019872103E-16));
#16813=DIRECTION('center_axis',(0.,1.83697019872103E-16,-1.));
#16814=DIRECTION('ref_axis',(0.,1.,2.09599627067876E-16));
#16815=DIRECTION('center_axis',(0.,1.83697019872103E-16,-1.));
#16816=DIRECTION('ref_axis',(0.,1.,1.83697019872103E-16));
#16817=DIRECTION('center_axis',(0.,1.83697019872103E-16,-1.));
#16818=DIRECTION('ref_axis',(0.,1.,1.83697019872103E-16));
#16819=DIRECTION('center_axis',(-1.,1.22464679914735E-16,2.24963967399279E-32));
#16820=DIRECTION('ref_axis',(-1.22464679914735E-16,-1.,-1.30999766917423E-16));
#16821=DIRECTION('center_axis',(0.,-1.83697019872103E-16,1.));
#16822=DIRECTION('ref_axis',(0.,1.,1.83697019872103E-16));
#16823=DIRECTION('center_axis',(0.,-1.83697019872103E-16,1.));
#16824=DIRECTION('ref_axis',(0.,1.,1.83697019872103E-16));
#16825=DIRECTION('center_axis',(0.,1.83697019872103E-16,-1.));
#16826=DIRECTION('ref_axis',(0.,1.,2.09599627067876E-16));
#16827=DIRECTION('center_axis',(0.,1.83697019872103E-16,-1.));
#16828=DIRECTION('ref_axis',(0.,1.,1.83697019872103E-16));
#16829=DIRECTION('center_axis',(0.,1.83697019872103E-16,-1.));
#16830=DIRECTION('ref_axis',(0.,1.,1.83697019872103E-16));
#16831=DIRECTION('center_axis',(-1.,1.22464679914735E-16,2.24963967399279E-32));
#16832=DIRECTION('ref_axis',(-1.22464679914735E-16,-1.,-1.30999766917423E-16));
#16833=DIRECTION('center_axis',(0.,-1.83697019872103E-16,1.));
#16834=DIRECTION('ref_axis',(0.,-1.,-1.83697019872103E-16));
#16835=DIRECTION('center_axis',(0.,-1.83697019872103E-16,1.));
#16836=DIRECTION('ref_axis',(0.,-1.,-1.83697019872103E-16));
#16837=DIRECTION('',(-8.65956056235483E-17,0.707106781186539,0.707106781186556));
#16838=DIRECTION('center_axis',(0.,-1.83697019872103E-16,1.));
#16839=DIRECTION('ref_axis',(0.,-1.,-1.83697019872103E-16));
#16840=DIRECTION('center_axis',(0.,-1.83697019872103E-16,1.));
#16841=DIRECTION('ref_axis',(0.,-1.,-1.83697019872103E-16));
#16842=DIRECTION('',(0.,-1.83697019872103E-16,1.));
#16843=DIRECTION('center_axis',(0.,1.83697019872103E-16,-1.));
#16844=DIRECTION('ref_axis',(0.,1.,1.83697019872103E-16));
#16845=DIRECTION('',(-8.65956056235483E-17,-0.707106781186539,-0.707106781186556));
#16846=DIRECTION('center_axis',(0.,-1.83697019872103E-16,1.));
#16847=DIRECTION('ref_axis',(0.,-1.,-1.83697019872103E-16));
#16848=DIRECTION('center_axis',(0.,-1.83697019872103E-16,1.));
#16849=DIRECTION('ref_axis',(0.,-1.,-1.83697019872103E-16));
#16850=DIRECTION('',(0.,1.83697019872103E-16,-1.));
#16851=DIRECTION('center_axis',(0.,-1.83697019872103E-16,1.));
#16852=DIRECTION('ref_axis',(0.,-1.,-1.83697019872103E-16));
#16853=DIRECTION('center_axis',(0.,-1.83697019872103E-16,1.));
#16854=DIRECTION('ref_axis',(0.,-1.,-1.83697019872103E-16));
#16855=DIRECTION('center_axis',(0.,-1.83697019872103E-16,1.));
#16856=DIRECTION('ref_axis',(0.,-1.,-1.83697019872103E-16));
#16857=DIRECTION('',(0.,1.83697019872103E-16,-1.));
#16858=DIRECTION('center_axis',(0.,1.83697019872103E-16,-1.));
#16859=DIRECTION('ref_axis',(0.,1.,1.83697019872103E-16));
#16860=DIRECTION('center_axis',(0.,-1.83697019872103E-16,1.));
#16861=DIRECTION('ref_axis',(0.,-1.,-1.83697019872103E-16));
#16862=DIRECTION('center_axis',(-1.,0.,0.));
#16863=DIRECTION('ref_axis',(0.,1.,0.));
#16864=DIRECTION('center_axis',(0.,1.22464679914735E-16,1.));
#16865=DIRECTION('ref_axis',(0.,-1.,1.22464679914735E-16));
#16866=DIRECTION('center_axis',(-0.623489801858732,0.781831482468031,1.43620113371566E-16));
#16867=DIRECTION('ref_axis',(0.781831482468031,0.623489801858732,-6.91638013500061E-17));
#16868=DIRECTION('center_axis',(2.39366855619276E-16,7.19167766472515E-18,
1.));
#16869=DIRECTION('ref_axis',(-0.781831482468031,-0.623489801858732,1.91628481264741E-16));
#16870=DIRECTION('center_axis',(0.222520933956319,0.974927912181823,1.79091352057932E-16));
#16871=DIRECTION('ref_axis',(0.974927912181823,-0.222520933956319,-2.24573452299036E-16));
#16872=DIRECTION('center_axis',(2.98485586763221E-16,-2.51824407250324E-16,
1.));
#16873=DIRECTION('ref_axis',(-0.974927912181823,0.222520933956319,3.47038132213772E-16));
#16874=DIRECTION('center_axis',(0.900968867902422,0.433883739117552,7.97031498468594E-17));
#16875=DIRECTION('ref_axis',(0.433883739117552,-0.900968867902422,-3.4920231590332E-16));
#16876=DIRECTION('center_axis',(1.32838583078098E-16,-4.59539179924132E-16,
1.));
#16877=DIRECTION('ref_axis',(-0.433883739117552,0.900968867902422,4.71666995818055E-16));
#16878=DIRECTION('center_axis',(0.900968867902416,-0.433883739117565,-7.97031498468616E-17));
#16879=DIRECTION('ref_axis',(-0.433883739117565,-0.900968867902416,-3.49202315903319E-16));
#16880=DIRECTION('center_axis',(-1.32838583078103E-16,-4.5953917992413E-16,
1.));
#16881=DIRECTION('ref_axis',(0.433883739117565,0.900968867902416,4.71666995818054E-16));
#16882=DIRECTION('center_axis',(0.222520933956305,-0.974927912181826,-1.79091352057933E-16));
#16883=DIRECTION('ref_axis',(-0.974927912181826,-0.222520933956305,-2.24573452299033E-16));
#16884=DIRECTION('center_axis',(-2.98485586763221E-16,-2.5182440725032E-16,
1.));
#16885=DIRECTION('ref_axis',(0.974927912181826,0.222520933956305,3.47038132213768E-16));
#16886=DIRECTION('center_axis',(-0.623489801858743,-0.781831482468022,-1.43620113371564E-16));
#16887=DIRECTION('ref_axis',(-0.781831482468022,0.623489801858743,-6.91638013500039E-17));
#16888=DIRECTION('center_axis',(-2.39366855619273E-16,7.19167766472869E-18,
1.));
#16889=DIRECTION('ref_axis',(0.781831482468022,-0.623489801858743,1.91628481264739E-16));
#16890=DIRECTION('center_axis',(0.,1.83697019872103E-16,-1.));
#16891=DIRECTION('ref_axis',(0.,1.,1.62614292875575E-16));
#16892=DIRECTION('center_axis',(0.,1.83697019872103E-16,-1.));
#16893=DIRECTION('ref_axis',(0.,1.,1.83697019872103E-16));
#16894=DIRECTION('center_axis',(-1.,1.22464679914735E-16,2.24963967399279E-32));
#16895=DIRECTION('ref_axis',(-1.22464679914735E-16,-1.,-2.03267866094469E-16));
#16896=DIRECTION('center_axis',(0.,-1.83697019872103E-16,1.));
#16897=DIRECTION('ref_axis',(0.,1.,1.83697019872103E-16));
#16898=DIRECTION('center_axis',(0.,-1.83697019872103E-16,1.));
#16899=DIRECTION('ref_axis',(0.,1.,1.83697019872103E-16));
#16900=DIRECTION('center_axis',(0.,-1.83697019872103E-16,1.));
#16901=DIRECTION('ref_axis',(0.,-1.,-1.64970202400831E-16));
#16902=DIRECTION('center_axis',(0.,-1.83697019872103E-16,1.));
#16903=DIRECTION('ref_axis',(0.,-1.,-1.83697019872103E-16));
#16904=DIRECTION('center_axis',(-1.,-1.22464679914735E-16,-2.24963967399279E-32));
#16905=DIRECTION('ref_axis',(-1.22464679914735E-16,1.,2.06212753001039E-16));
#16906=DIRECTION('center_axis',(0.,1.83697019872103E-16,-1.));
#16907=DIRECTION('ref_axis',(0.,-1.,-1.83697019872103E-16));
#16908=DIRECTION('center_axis',(0.,-1.83697019872103E-16,1.));
#16909=DIRECTION('ref_axis',(0.,-1.,-1.62614292875575E-16));
#16910=DIRECTION('center_axis',(0.,-1.83697019872103E-16,1.));
#16911=DIRECTION('ref_axis',(0.,-1.,-1.83697019872103E-16));
#16912=DIRECTION('center_axis',(-1.,-1.22464679914735E-16,-2.24963967399279E-32));
#16913=DIRECTION('ref_axis',(-1.22464679914735E-16,1.,2.03267866094469E-16));
#16914=DIRECTION('center_axis',(0.,1.83697019872103E-16,-1.));
#16915=DIRECTION('ref_axis',(0.,-1.,-1.83697019872103E-16));
#16916=DIRECTION('center_axis',(0.,1.83697019872103E-16,-1.));
#16917=DIRECTION('ref_axis',(0.,1.,1.64970202400831E-16));
#16918=DIRECTION('center_axis',(0.,1.83697019872103E-16,-1.));
#16919=DIRECTION('ref_axis',(0.,1.,1.83697019872103E-16));
#16920=DIRECTION('center_axis',(0.,1.83697019872103E-16,-1.));
#16921=DIRECTION('ref_axis',(0.,1.,1.83697019872103E-16));
#16922=DIRECTION('center_axis',(-1.,1.22464679914735E-16,2.24963967399279E-32));
#16923=DIRECTION('ref_axis',(-1.22464679914735E-16,-1.,-2.06212753001039E-16));
#16924=DIRECTION('center_axis',(0.,-1.83697019872103E-16,1.));
#16925=DIRECTION('ref_axis',(0.,1.,1.83697019872103E-16));
#16926=DIRECTION('center_axis',(0.,-1.83697019872103E-16,1.));
#16927=DIRECTION('ref_axis',(0.,-1.,-1.83697019872103E-16));
#16928=DIRECTION('center_axis',(0.,-1.83697019872103E-16,1.));
#16929=DIRECTION('ref_axis',(0.,-1.,-1.83697019872103E-16));
#16930=DIRECTION('',(0.,-1.83697019872103E-16,1.));
#16931=DIRECTION('center_axis',(0.,-1.83697019872103E-16,1.));
#16932=DIRECTION('ref_axis',(0.,-1.,-1.83697019872103E-16));
#16933=DIRECTION('center_axis',(0.,-1.83697019872103E-16,1.));
#16934=DIRECTION('ref_axis',(0.,-1.,-1.83697019872103E-16));
#16935=DIRECTION('center_axis',(0.,-1.83697019872103E-16,1.));
#16936=DIRECTION('ref_axis',(0.,-1.,-1.83697019872103E-16));
#16937=DIRECTION('',(0.,-1.83697019872103E-16,1.));
#16938=DIRECTION('center_axis',(0.,-1.83697019872103E-16,1.));
#16939=DIRECTION('ref_axis',(0.,-1.,-1.83697019872103E-16));
#16940=DIRECTION('',(0.,-1.83697019872103E-16,1.));
#16941=DIRECTION('center_axis',(0.,-1.83697019872103E-16,1.));
#16942=DIRECTION('ref_axis',(0.,-1.,-1.83697019872103E-16));
#16943=DIRECTION('center_axis',(0.,-1.83697019872103E-16,1.));
#16944=DIRECTION('ref_axis',(0.,-1.,-1.83697019872103E-16));
#16945=DIRECTION('center_axis',(1.,1.22464679914735E-16,2.24963967399279E-32));
#16946=DIRECTION('ref_axis',(-1.22464679914735E-16,1.,1.83697019872103E-16));
#16947=DIRECTION('center_axis',(0.,-1.83697019872103E-16,1.));
#16948=DIRECTION('ref_axis',(0.,-1.,-1.83697019872103E-16));
#16949=DIRECTION('center_axis',(0.,-1.83697019872103E-16,1.));
#16950=DIRECTION('ref_axis',(0.,-1.,-1.83697019872103E-16));
#16951=DIRECTION('',(0.,-1.83697019872103E-16,1.));
#16952=DIRECTION('center_axis',(0.,-1.83697019872103E-16,1.));
#16953=DIRECTION('ref_axis',(0.,-1.,-1.83697019872103E-16));
#16954=DIRECTION('',(0.,-1.83697019872103E-16,1.));
#16955=DIRECTION('center_axis',(0.,-1.83697019872103E-16,1.));
#16956=DIRECTION('ref_axis',(0.,-1.,-1.83697019872103E-16));
#16957=DIRECTION('center_axis',(0.,-1.83697019872103E-16,1.));
#16958=DIRECTION('ref_axis',(0.,-1.,-1.83697019872103E-16));
#16959=DIRECTION('center_axis',(0.,-1.83697019872103E-16,1.));
#16960=DIRECTION('ref_axis',(0.,-1.,-1.83697019872103E-16));
#16961=DIRECTION('',(0.,-1.83697019872103E-16,1.));
#16962=DIRECTION('center_axis',(0.,-1.83697019872103E-16,1.));
#16963=DIRECTION('ref_axis',(0.,-1.,-1.83697019872103E-16));
#16964=DIRECTION('center_axis',(0.,-1.83697019872103E-16,1.));
#16965=DIRECTION('ref_axis',(0.,-1.,-1.83697019872103E-16));
#16966=DIRECTION('center_axis',(0.,-1.83697019872103E-16,1.));
#16967=DIRECTION('ref_axis',(0.,-1.,-1.83697019872103E-16));
#16968=DIRECTION('',(8.65956056235488E-17,-0.707106781186543,-0.707106781186552));
#16969=DIRECTION('center_axis',(0.,-1.83697019872103E-16,1.));
#16970=DIRECTION('ref_axis',(0.,-1.,-1.83697019872103E-16));
#16971=DIRECTION('center_axis',(0.,1.83697019872103E-16,-1.));
#16972=DIRECTION('ref_axis',(0.,1.,1.83697019872103E-16));
#16973=DIRECTION('center_axis',(0.,-1.83697019872103E-16,1.));
#16974=DIRECTION('ref_axis',(0.,-1.,-1.83697019872103E-16));
#16975=DIRECTION('',(8.65956056235488E-17,0.707106781186543,0.707106781186552));
#16976=DIRECTION('center_axis',(0.,-1.83697019872103E-16,1.));
#16977=DIRECTION('ref_axis',(0.,-1.,-1.83697019872103E-16));
#16978=DIRECTION('center_axis',(0.,-1.83697019872103E-16,1.));
#16979=DIRECTION('ref_axis',(0.,-1.,-1.83697019872103E-16));
#16980=DIRECTION('center_axis',(0.,-1.83697019872103E-16,1.));
#16981=DIRECTION('ref_axis',(0.,-1.,-1.83697019872103E-16));
#16982=DIRECTION('',(0.,1.83697019872103E-16,-1.));
#16983=DIRECTION('center_axis',(0.,1.83697019872103E-16,-1.));
#16984=DIRECTION('ref_axis',(0.,1.,1.83697019872103E-16));
#16985=DIRECTION('center_axis',(0.,-1.83697019872103E-16,1.));
#16986=DIRECTION('ref_axis',(0.,-1.,-1.83697019872103E-16));
#16987=DIRECTION('center_axis',(0.,1.83697019872103E-16,-1.));
#16988=DIRECTION('ref_axis',(0.,1.,1.83697019872103E-16));
#16989=DIRECTION('center_axis',(0.,-1.83697019872103E-16,1.));
#16990=DIRECTION('ref_axis',(0.,-1.,-1.83697019872103E-16));
#16991=DIRECTION('center_axis',(0.,1.83697019872103E-16,-1.));
#16992=DIRECTION('ref_axis',(0.,1.,1.83697019872103E-16));
#16993=DIRECTION('center_axis',(0.,-1.83697019872103E-16,1.));
#16994=DIRECTION('ref_axis',(0.,-1.,-1.83697019872103E-16));
#16995=DIRECTION('center_axis',(-0.781831482468031,0.623489801858732,-6.91638013500059E-17));
#16996=DIRECTION('ref_axis',(0.,0.,1.));
#16997=DIRECTION('center_axis',(-0.781831482468031,0.623489801858732,-6.91638013500059E-17));
#16998=DIRECTION('ref_axis',(-5.40744373425995E-17,4.31229247995119E-17,
1.));
#16999=DIRECTION('center_axis',(-0.623489801858732,-0.781831482468031,2.05955304247937E-16));
#17000=DIRECTION('ref_axis',(0.,-2.63426721571497E-16,-1.));
#17001=DIRECTION('center_axis',(-0.781831482468031,0.623489801858732,-6.91638013500059E-17));
#17002=DIRECTION('ref_axis',(-5.40744373425995E-17,4.31229247995119E-17,
1.));
#17003=DIRECTION('center_axis',(0.623489801858732,0.781831482468031,1.22464679914735E-16));
#17004=DIRECTION('ref_axis',(0.,0.,1.));
#17005=DIRECTION('center_axis',(-1.79091352057932E-16,-2.24573452299036E-16,
1.));
#17006=DIRECTION('ref_axis',(-5.50003967499518E-33,-1.,-2.24573452299036E-16));
#17007=DIRECTION('center_axis',(0.781831482468031,-0.623489801858732,0.));
#17008=DIRECTION('ref_axis',(0.,0.,-1.));
#17009=DIRECTION('center_axis',(-1.43620113371566E-16,-6.91638013500059E-17,
1.));
#17010=DIRECTION('ref_axis',(0.623489801858732,0.781831482468031,1.43620113371566E-16));
#17011=DIRECTION('center_axis',(-1.43620113371566E-16,-6.91638013500059E-17,
1.));
#17012=DIRECTION('ref_axis',(0.623489801858732,0.781831482468031,1.43620113371566E-16));
#17013=DIRECTION('center_axis',(-1.43620113371566E-16,-6.91638013500059E-17,
1.));
#17014=DIRECTION('ref_axis',(0.623489801858732,0.781831482468031,1.43620113371566E-16));
#17015=DIRECTION('center_axis',(-1.79091352057932E-16,-2.24573452299036E-16,
1.));
#17016=DIRECTION('ref_axis',(-5.50003967499518E-33,-1.,-2.24573452299036E-16));
#17017=DIRECTION('center_axis',(-1.79091352057932E-16,-2.24573452299036E-16,
1.));
#17018=DIRECTION('ref_axis',(-5.5000396749952E-33,-1.,-2.24573452299036E-16));
#17019=DIRECTION('center_axis',(-0.781831482468031,0.623489801858732,-6.91638013500059E-17));
#17020=DIRECTION('ref_axis',(-5.40744373425995E-17,4.31229247995119E-17,
1.));
#17021=DIRECTION('center_axis',(-0.781831482468031,0.623489801858732,-6.91638013500059E-17));
#17022=DIRECTION('ref_axis',(-5.40744373425995E-17,4.31229247995119E-17,
1.));
#17023=DIRECTION('center_axis',(-0.974927912181823,-0.222520933956318,-2.24573452299036E-16));
#17024=DIRECTION('ref_axis',(0.,-2.10741377257197E-16,1.));
#17025=DIRECTION('center_axis',(-0.974927912181823,-0.222520933956318,-2.24573452299036E-16));
#17026=DIRECTION('ref_axis',(-1.71433215598957E-16,-2.58125940401653E-16,
1.));
#17027=DIRECTION('center_axis',(0.222520933956318,-0.974927912181823,-1.28411031837301E-16));
#17028=DIRECTION('ref_axis',(0.,1.31713360785748E-16,-1.));
#17029=DIRECTION('center_axis',(-0.974927912181823,-0.222520933956318,-2.24573452299036E-16));
#17030=DIRECTION('ref_axis',(-1.71433215598957E-16,-2.58125940401653E-16,
1.));
#17031=DIRECTION('center_axis',(-0.222520933956318,0.974927912181823,3.59586625308286E-16));
#17032=DIRECTION('ref_axis',(0.,-2.4905725751517E-16,1.));
#17033=DIRECTION('center_axis',(-7.97031498468594E-17,-3.4920231590332E-16,
1.));
#17034=DIRECTION('ref_axis',(2.39882519785021E-33,-1.,-3.4920231590332E-16));
#17035=DIRECTION('center_axis',(0.974927912181823,0.222520933956318,6.92755669385935E-17));
#17036=DIRECTION('ref_axis',(0.,3.11321571893962E-16,-1.));
#17037=DIRECTION('center_axis',(-1.79091352057932E-16,-2.24573452299036E-16,
1.));
#17038=DIRECTION('ref_axis',(-0.222520933956318,0.974927912181823,1.79091352057933E-16));
#17039=DIRECTION('center_axis',(-1.79091352057932E-16,-2.24573452299036E-16,
1.));
#17040=DIRECTION('ref_axis',(-0.222520933956318,0.974927912181823,1.79091352057933E-16));
#17041=DIRECTION('center_axis',(-1.79091352057932E-16,-2.24573452299036E-16,
1.));
#17042=DIRECTION('ref_axis',(-0.222520933956318,0.974927912181823,1.79091352057933E-16));
#17043=DIRECTION('center_axis',(-7.97031498468594E-17,-3.4920231590332E-16,
1.));
#17044=DIRECTION('ref_axis',(2.39882519785021E-33,-1.,-3.4920231590332E-16));
#17045=DIRECTION('center_axis',(-7.97031498468594E-17,-3.4920231590332E-16,
1.));
#17046=DIRECTION('ref_axis',(2.39882519785021E-33,-1.,-3.4920231590332E-16));
#17047=DIRECTION('center_axis',(-0.974927912181823,-0.222520933956318,-2.24573452299036E-16));
#17048=DIRECTION('ref_axis',(-1.64444757441796E-16,-2.88744376156862E-16,
1.));
#17049=DIRECTION('center_axis',(-0.974927912181823,-0.222520933956318,-2.24573452299036E-16));
#17050=DIRECTION('ref_axis',(-1.64444757441796E-16,-2.88744376156862E-16,
1.));
#17051=DIRECTION('center_axis',(-0.433883739117553,-0.900968867902422,-3.4920231590332E-16));
#17052=DIRECTION('ref_axis',(0.,-4.21482754514395E-16,1.));
#17053=DIRECTION('center_axis',(-0.433883739117553,-0.900968867902422,-3.4920231590332E-16));
#17054=DIRECTION('ref_axis',(1.97058769816641E-17,-3.97075180104293E-16,
1.));
#17055=DIRECTION('center_axis',(0.900968867902422,-0.433883739117553,-2.28593141877839E-16));
#17056=DIRECTION('ref_axis',(0.,5.26853443142994E-16,-1.));
#17057=DIRECTION('center_axis',(-0.433883739117553,-0.900968867902422,-3.4920231590332E-16));
#17058=DIRECTION('ref_axis',(1.97058769816641E-17,-3.97075180104293E-16,
1.));
#17059=DIRECTION('center_axis',(-0.900968867902422,0.433883739117552,3.33523066916777E-16));
#17060=DIRECTION('ref_axis',(0.,-4.9811451503034E-16,1.));
#17061=DIRECTION('center_axis',(7.97031498468617E-17,-3.49202315903319E-16,
1.));
#17062=DIRECTION('ref_axis',(-2.39882519785018E-33,-1.,-3.49202315903319E-16));
#17063=DIRECTION('center_axis',(0.433883739117552,0.900968867902422,5.60982088365811E-16));
#17064=DIRECTION('ref_axis',(0.,6.22643143787925E-16,-1.));
#17065=DIRECTION('center_axis',(-7.97031498468594E-17,-3.4920231590332E-16,
1.));
#17066=DIRECTION('ref_axis',(-0.900968867902422,0.433883739117553,7.97031498468594E-17));
#17067=DIRECTION('center_axis',(-7.97031498468594E-17,-3.4920231590332E-16,
1.));
#17068=DIRECTION('ref_axis',(-0.900968867902422,0.433883739117553,7.97031498468594E-17));
#17069=DIRECTION('center_axis',(-7.97031498468594E-17,-3.4920231590332E-16,
1.));
#17070=DIRECTION('ref_axis',(-0.900968867902422,0.433883739117553,7.97031498468594E-17));
#17071=DIRECTION('center_axis',(7.97031498468617E-17,-3.49202315903319E-16,
1.));
#17072=DIRECTION('ref_axis',(-2.39882519785018E-33,-1.,-3.49202315903319E-16));
#17073=DIRECTION('center_axis',(7.97031498468617E-17,-3.49202315903319E-16,
1.));
#17074=DIRECTION('ref_axis',(-2.39882519785018E-33,-1.,-3.49202315903319E-16));
#17075=DIRECTION('center_axis',(-0.433883739117553,-0.900968867902422,-3.4920231590332E-16));
#17076=DIRECTION('ref_axis',(4.4891409918625E-17,-4.09203893527874E-16,
1.));
#17077=DIRECTION('center_axis',(-0.433883739117553,-0.900968867902422,-3.4920231590332E-16));
#17078=DIRECTION('ref_axis',(4.48914099186251E-17,-4.09203893527874E-16,
1.));
#17079=DIRECTION('center_axis',(0.433883739117565,-0.900968867902416,-3.49202315903319E-16));
#17080=DIRECTION('ref_axis',(0.,-4.21482754514395E-16,1.));
#17081=DIRECTION('center_axis',(0.433883739117565,-0.900968867902416,-3.49202315903319E-16));
#17082=DIRECTION('ref_axis',(-1.97058769816642E-17,-3.97075180104295E-16,
1.));
#17083=DIRECTION('center_axis',(0.900968867902416,0.433883739117565,2.28593141877845E-16));
#17084=DIRECTION('ref_axis',(0.,5.26853443142994E-16,-1.));
#17085=DIRECTION('center_axis',(0.433883739117565,-0.900968867902416,-3.49202315903319E-16));
#17086=DIRECTION('ref_axis',(-1.97058769816642E-17,-3.97075180104295E-16,
1.));
#17087=DIRECTION('center_axis',(-0.900968867902416,-0.433883739117565,-8.85937070873124E-17));
#17088=DIRECTION('ref_axis',(0.,-4.9811451503034E-16,1.));
#17089=DIRECTION('center_axis',(1.79091352057933E-16,-2.24573452299033E-16,
1.));
#17090=DIRECTION('ref_axis',(5.50003967499563E-33,-1.,-2.24573452299033E-16));
#17091=DIRECTION('center_axis',(-0.433883739117565,0.900968867902416,5.60982088365808E-16));
#17092=DIRECTION('ref_axis',(0.,6.22643143787925E-16,-1.));
#17093=DIRECTION('center_axis',(7.97031498468617E-17,-3.49202315903319E-16,
1.));
#17094=DIRECTION('ref_axis',(-0.900968867902416,-0.433883739117565,-7.97031498468616E-17));
#17095=DIRECTION('center_axis',(7.97031498468617E-17,-3.49202315903319E-16,
1.));
#17096=DIRECTION('ref_axis',(-0.900968867902416,-0.433883739117565,-7.97031498468616E-17));
#17097=DIRECTION('center_axis',(7.97031498468617E-17,-3.49202315903319E-16,
1.));
#17098=DIRECTION('ref_axis',(-0.900968867902416,-0.433883739117565,-7.97031498468616E-17));
#17099=DIRECTION('center_axis',(1.79091352057933E-16,-2.24573452299033E-16,
1.));
#17100=DIRECTION('ref_axis',(5.50003967499563E-33,-1.,-2.24573452299033E-16));
#17101=DIRECTION('center_axis',(1.79091352057933E-16,-2.24573452299033E-16,
1.));
#17102=DIRECTION('ref_axis',(5.50003967499563E-33,-1.,-2.24573452299033E-16));
#17103=DIRECTION('center_axis',(0.433883739117565,-0.900968867902416,-3.49202315903319E-16));
#17104=DIRECTION('ref_axis',(-4.48914099186257E-17,-4.09203893527877E-16,
1.));
#17105=DIRECTION('center_axis',(0.433883739117565,-0.900968867902416,-3.49202315903319E-16));
#17106=DIRECTION('ref_axis',(-4.48914099186258E-17,-4.09203893527877E-16,
1.));
#17107=DIRECTION('center_axis',(0.974927912181826,-0.222520933956305,-2.24573452299033E-16));
#17108=DIRECTION('ref_axis',(0.,-2.10741377257197E-16,1.));
#17109=DIRECTION('center_axis',(0.974927912181826,-0.222520933956305,-2.24573452299033E-16));
#17110=DIRECTION('ref_axis',(1.71433215598957E-16,-2.58125940401651E-16,
1.));
#17111=DIRECTION('center_axis',(0.222520933956305,0.974927912181826,3.85233095511904E-16));
#17112=DIRECTION('ref_axis',(0.,3.95140082357245E-16,-1.));
#17113=DIRECTION('center_axis',(0.974927912181826,-0.222520933956305,-2.24573452299033E-16));
#17114=DIRECTION('ref_axis',(1.71433215598957E-16,-2.58125940401651E-16,
1.));
#17115=DIRECTION('center_axis',(-0.222520933956305,-0.974927912181826,-1.14657265478815E-16));
#17116=DIRECTION('ref_axis',(0.,-1.24528628757585E-16,1.));
#17117=DIRECTION('center_axis',(1.43620113371564E-16,-6.91638013500039E-17,
1.));
#17118=DIRECTION('ref_axis',(1.,1.10509814492259E-33,-1.43620113371564E-16));
#17119=DIRECTION('center_axis',(-0.974927912181826,0.222520933956305,3.46377834692947E-17));
#17120=DIRECTION('ref_axis',(0.,1.55660785946981E-16,-1.));
#17121=DIRECTION('center_axis',(1.79091352057933E-16,-2.24573452299033E-16,
1.));
#17122=DIRECTION('ref_axis',(-0.222520933956305,-0.974927912181826,-1.79091352057932E-16));
#17123=DIRECTION('center_axis',(1.79091352057933E-16,-2.24573452299033E-16,
1.));
#17124=DIRECTION('ref_axis',(-0.222520933956305,-0.974927912181826,-1.79091352057932E-16));
#17125=DIRECTION('center_axis',(1.79091352057933E-16,-2.24573452299033E-16,
1.));
#17126=DIRECTION('ref_axis',(-0.222520933956305,-0.974927912181826,-1.79091352057932E-16));
#17127=DIRECTION('center_axis',(1.43620113371564E-16,-6.91638013500039E-17,
1.));
#17128=DIRECTION('ref_axis',(1.,1.10509814492259E-33,-1.43620113371564E-16));
#17129=DIRECTION('center_axis',(1.43620113371564E-16,-6.91638013500039E-17,
1.));
#17130=DIRECTION('ref_axis',(1.,1.10509814492259E-33,-1.43620113371564E-16));
#17131=DIRECTION('center_axis',(0.974927912181826,-0.222520933956305,-2.24573452299033E-16));
#17132=DIRECTION('ref_axis',(1.64444757441797E-16,-2.8874437615686E-16,
1.));
#17133=DIRECTION('center_axis',(0.974927912181826,-0.222520933956305,-2.24573452299033E-16));
#17134=DIRECTION('ref_axis',(1.64444757441797E-16,-2.8874437615686E-16,
1.));
#17135=DIRECTION('center_axis',(0.781831482468022,0.623489801858743,-6.91638013500039E-17));
#17136=DIRECTION('ref_axis',(0.,0.,1.));
#17137=DIRECTION('center_axis',(0.781831482468022,0.623489801858743,-6.91638013500039E-17));
#17138=DIRECTION('ref_axis',(5.40744373425973E-17,4.31229247995114E-17,
1.));
#17139=DIRECTION('center_axis',(-0.623489801858743,0.781831482468022,0.));
#17140=DIRECTION('ref_axis',(0.,0.,-1.));
#17141=DIRECTION('center_axis',(0.781831482468022,0.623489801858743,-6.91638013500039E-17));
#17142=DIRECTION('ref_axis',(5.40744373425973E-17,4.31229247995114E-17,
1.));
#17143=DIRECTION('center_axis',(0.623489801858743,-0.781831482468022,1.22464679914735E-16));
#17144=DIRECTION('ref_axis',(0.,0.,1.));
#17145=DIRECTION('center_axis',(0.,0.,-1.));
#17146=DIRECTION('ref_axis',(1.,0.,0.));
#17147=DIRECTION('center_axis',(0.,0.,-1.));
#17148=DIRECTION('ref_axis',(1.,0.,0.));
#17149=DIRECTION('center_axis',(0.,0.,-1.));
#17150=DIRECTION('ref_axis',(1.,0.,0.));
#17151=DIRECTION('center_axis',(-0.781831482468022,-0.623489801858743,0.));
#17152=DIRECTION('ref_axis',(0.,0.,-1.));
#17153=DIRECTION('center_axis',(1.43620113371564E-16,-6.91638013500039E-17,
1.));
#17154=DIRECTION('ref_axis',(0.623489801858743,-0.781831482468022,-1.43620113371564E-16));
#17155=DIRECTION('center_axis',(1.43620113371564E-16,-6.91638013500039E-17,
1.));
#17156=DIRECTION('ref_axis',(0.623489801858743,-0.781831482468022,-1.43620113371564E-16));
#17157=DIRECTION('center_axis',(1.43620113371564E-16,-6.91638013500039E-17,
1.));
#17158=DIRECTION('ref_axis',(0.623489801858743,-0.781831482468022,-1.43620113371564E-16));
#17159=DIRECTION('center_axis',(0.781831482468022,0.623489801858743,-6.91638013500039E-17));
#17160=DIRECTION('ref_axis',(5.40744373425973E-17,4.31229247995114E-17,
1.));
#17161=DIRECTION('center_axis',(0.781831482468022,0.623489801858743,-6.91638013500039E-17));
#17162=DIRECTION('ref_axis',(5.40744373425973E-17,4.31229247995114E-17,
1.));
#17163=DIRECTION('center_axis',(1.,0.,1.22464679914735E-16));
#17164=DIRECTION('ref_axis',(-6.12323399573677E-17,0.,1.));
#17165=DIRECTION('center_axis',(-1.43620113371566E-16,-6.91638013500059E-17,
1.));
#17166=DIRECTION('ref_axis',(1.,-1.10509814492274E-33,1.43620113371566E-16));
#17167=DIRECTION('center_axis',(0.,-1.,0.));
#17168=DIRECTION('ref_axis',(6.12323399573677E-17,0.,-1.));
#17169=DIRECTION('center_axis',(0.,0.,1.));
#17170=DIRECTION('ref_axis',(1.,0.,0.));
#17171=DIRECTION('center_axis',(0.,0.,1.));
#17172=DIRECTION('ref_axis',(1.,0.,0.));
#17173=DIRECTION('center_axis',(0.,0.,1.));
#17174=DIRECTION('ref_axis',(1.,0.,0.));
#17175=DIRECTION('center_axis',(-1.43620113371566E-16,-6.91638013500059E-17,
1.));
#17176=DIRECTION('ref_axis',(1.,-1.10509814492274E-33,1.43620113371566E-16));
#17177=DIRECTION('center_axis',(-1.43620113371566E-16,-6.91638013500059E-17,
1.));
#17178=DIRECTION('ref_axis',(1.,-1.10509814492274E-33,1.43620113371566E-16));
#17179=DIRECTION('center_axis',(0.,1.,0.));
#17180=DIRECTION('ref_axis',(0.,0.,1.));
#17181=DIRECTION('center_axis',(0.,1.,0.));
#17182=DIRECTION('ref_axis',(0.,0.,1.));
#17183=DIRECTION('center_axis',(0.,1.,0.));
#17184=DIRECTION('ref_axis',(0.,0.,1.));
#17185=DIRECTION('center_axis',(0.,1.,0.));
#17186=DIRECTION('ref_axis',(0.,0.,1.));
#17187=DIRECTION('center_axis',(-1.,0.,1.22464679914735E-16));
#17188=DIRECTION('ref_axis',(-1.22464679914735E-16,0.,-1.));
#17189=DIRECTION('center_axis',(0.,1.,0.));
#17190=DIRECTION('ref_axis',(0.,0.,1.));
#17191=DIRECTION('center_axis',(0.,0.,-1.));
#17192=DIRECTION('ref_axis',(-1.,0.,0.));
#17193=DIRECTION('center_axis',(0.,0.,-1.));
#17194=DIRECTION('ref_axis',(1.,0.,0.));
#17195=DIRECTION('center_axis',(0.,0.,-1.));
#17196=DIRECTION('ref_axis',(1.,0.,0.));
#17197=DIRECTION('center_axis',(0.,0.,-1.));
#17198=DIRECTION('ref_axis',(-1.,0.,0.));
#17199=DIRECTION('center_axis',(0.,0.,1.));
#17200=DIRECTION('ref_axis',(1.,0.,0.));
#17201=DIRECTION('center_axis',(0.,0.,1.));
#17202=DIRECTION('ref_axis',(1.,0.,0.));
#17203=DIRECTION('center_axis',(0.,0.,1.));
#17204=DIRECTION('ref_axis',(1.,0.,0.));
#17205=DIRECTION('center_axis',(0.,0.,1.));
#17206=DIRECTION('ref_axis',(1.,0.,0.));
#17207=DIRECTION('center_axis',(0.,1.,0.));
#17208=DIRECTION('ref_axis',(0.,0.,1.));
#17209=DIRECTION('center_axis',(0.,-1.,0.));
#17210=DIRECTION('ref_axis',(0.,0.,-1.));
#17211=DIRECTION('center_axis',(0.,0.,1.));
#17212=DIRECTION('ref_axis',(1.,0.,0.));
#17213=DIRECTION('center_axis',(0.,0.,-1.));
#17214=DIRECTION('ref_axis',(1.,0.,0.));
#17215=DIRECTION('center_axis',(0.,0.,1.));
#17216=DIRECTION('ref_axis',(1.,0.,0.));
#17217=DIRECTION('center_axis',(0.,0.,1.));
#17218=DIRECTION('ref_axis',(1.,0.,0.));
#17219=DIRECTION('center_axis',(0.,0.,-1.));
#17220=DIRECTION('ref_axis',(1.,0.,0.));
#17221=DIRECTION('center_axis',(0.,0.,1.));
#17222=DIRECTION('ref_axis',(1.,0.,0.));
#17223=DIRECTION('center_axis',(0.,0.,-1.));
#17224=DIRECTION('ref_axis',(-1.,0.,0.));
#17225=DIRECTION('center_axis',(0.,0.,-1.));
#17226=DIRECTION('ref_axis',(-1.,0.,0.));
#17227=DIRECTION('center_axis',(-0.781831482468022,-0.623489801858743,6.91638013500039E-17));
#17228=DIRECTION('ref_axis',(-1.43620113371564E-16,6.91638013500039E-17,
-1.));
#17229=DIRECTION('center_axis',(0.781831482468022,0.623489801858743,-6.91638013500039E-17));
#17230=DIRECTION('ref_axis',(1.43620113371564E-16,-6.91638013500039E-17,
1.));
#17231=DIRECTION('center_axis',(1.43620113371564E-16,-6.91638013500039E-17,
1.));
#17232=DIRECTION('ref_axis',(0.623489801858743,-0.781831482468022,-1.43620113371564E-16));
#17233=DIRECTION('center_axis',(-1.43620113371564E-16,6.91638013500039E-17,
-1.));
#17234=DIRECTION('ref_axis',(0.623489801858743,-0.781831482468022,-1.43620113371564E-16));
#17235=DIRECTION('center_axis',(1.43620113371564E-16,-6.91638013500039E-17,
1.));
#17236=DIRECTION('ref_axis',(0.623489801858743,-0.781831482468022,-1.43620113371564E-16));
#17237=DIRECTION('center_axis',(1.43620113371564E-16,-6.91638013500039E-17,
1.));
#17238=DIRECTION('ref_axis',(0.623489801858743,-0.781831482468022,-1.43620113371564E-16));
#17239=DIRECTION('center_axis',(-1.43620113371564E-16,6.91638013500039E-17,
-1.));
#17240=DIRECTION('ref_axis',(0.623489801858743,-0.781831482468022,-1.43620113371564E-16));
#17241=DIRECTION('center_axis',(1.43620113371564E-16,-6.91638013500039E-17,
1.));
#17242=DIRECTION('ref_axis',(0.623489801858743,-0.781831482468022,-1.43620113371564E-16));
#17243=DIRECTION('center_axis',(-1.43620113371564E-16,6.91638013500039E-17,
-1.));
#17244=DIRECTION('ref_axis',(-0.623489801858743,0.781831482468022,1.43620113371564E-16));
#17245=DIRECTION('center_axis',(-1.43620113371564E-16,6.91638013500039E-17,
-1.));
#17246=DIRECTION('ref_axis',(-0.623489801858743,0.781831482468022,1.43620113371564E-16));
#17247=DIRECTION('center_axis',(-1.79091352057933E-16,2.24573452299033E-16,
-1.));
#17248=DIRECTION('ref_axis',(0.222520933956305,0.974927912181826,1.79091352057932E-16));
#17249=DIRECTION('center_axis',(-1.79091352057933E-16,2.24573452299033E-16,
-1.));
#17250=DIRECTION('ref_axis',(-0.222520933956305,-0.974927912181826,-1.79091352057932E-16));
#17251=DIRECTION('center_axis',(-1.79091352057933E-16,2.24573452299033E-16,
-1.));
#17252=DIRECTION('ref_axis',(-0.222520933956305,-0.974927912181826,-1.79091352057932E-16));
#17253=DIRECTION('center_axis',(-1.79091352057933E-16,2.24573452299033E-16,
-1.));
#17254=DIRECTION('ref_axis',(0.222520933956305,0.974927912181826,1.79091352057932E-16));
#17255=DIRECTION('center_axis',(1.79091352057933E-16,-2.24573452299033E-16,
1.));
#17256=DIRECTION('ref_axis',(-0.222520933956305,-0.974927912181826,-1.79091352057932E-16));
#17257=DIRECTION('center_axis',(1.79091352057933E-16,-2.24573452299033E-16,
1.));
#17258=DIRECTION('ref_axis',(-0.222520933956305,-0.974927912181826,-1.79091352057932E-16));
#17259=DIRECTION('center_axis',(1.79091352057933E-16,-2.24573452299033E-16,
1.));
#17260=DIRECTION('ref_axis',(-0.222520933956305,-0.974927912181826,-1.79091352057932E-16));
#17261=DIRECTION('center_axis',(1.79091352057933E-16,-2.24573452299033E-16,
1.));
#17262=DIRECTION('ref_axis',(-0.222520933956305,-0.974927912181826,-1.79091352057932E-16));
#17263=DIRECTION('center_axis',(-0.974927912181826,0.222520933956305,2.24573452299033E-16));
#17264=DIRECTION('ref_axis',(-1.79091352057933E-16,2.24573452299033E-16,
-1.));
#17265=DIRECTION('center_axis',(0.974927912181826,-0.222520933956305,-2.24573452299033E-16));
#17266=DIRECTION('ref_axis',(1.79091352057933E-16,-2.24573452299033E-16,
1.));
#17267=DIRECTION('center_axis',(1.79091352057933E-16,-2.24573452299033E-16,
1.));
#17268=DIRECTION('ref_axis',(-0.222520933956305,-0.974927912181826,-1.79091352057932E-16));
#17269=DIRECTION('center_axis',(-1.79091352057933E-16,2.24573452299033E-16,
-1.));
#17270=DIRECTION('ref_axis',(-0.222520933956305,-0.974927912181826,-1.79091352057932E-16));
#17271=DIRECTION('center_axis',(1.79091352057933E-16,-2.24573452299033E-16,
1.));
#17272=DIRECTION('ref_axis',(-0.222520933956305,-0.974927912181826,-1.79091352057932E-16));
#17273=DIRECTION('center_axis',(1.79091352057933E-16,-2.24573452299033E-16,
1.));
#17274=DIRECTION('ref_axis',(-0.222520933956305,-0.974927912181826,-1.79091352057932E-16));
#17275=DIRECTION('center_axis',(-1.79091352057933E-16,2.24573452299033E-16,
-1.));
#17276=DIRECTION('ref_axis',(-0.222520933956305,-0.974927912181826,-1.79091352057932E-16));
#17277=DIRECTION('center_axis',(1.79091352057933E-16,-2.24573452299033E-16,
1.));
#17278=DIRECTION('ref_axis',(-0.222520933956305,-0.974927912181826,-1.79091352057932E-16));
#17279=DIRECTION('center_axis',(-1.79091352057933E-16,2.24573452299033E-16,
-1.));
#17280=DIRECTION('ref_axis',(0.222520933956305,0.974927912181826,1.79091352057932E-16));
#17281=DIRECTION('center_axis',(-1.79091352057933E-16,2.24573452299033E-16,
-1.));
#17282=DIRECTION('ref_axis',(0.222520933956305,0.974927912181826,1.79091352057932E-16));
#17283=DIRECTION('center_axis',(-7.97031498468617E-17,3.49202315903319E-16,
-1.));
#17284=DIRECTION('ref_axis',(0.900968867902416,0.433883739117565,7.97031498468616E-17));
#17285=DIRECTION('center_axis',(-7.97031498468617E-17,3.49202315903319E-16,
-1.));
#17286=DIRECTION('ref_axis',(-0.900968867902416,-0.433883739117565,-7.97031498468616E-17));
#17287=DIRECTION('center_axis',(-7.97031498468617E-17,3.49202315903319E-16,
-1.));
#17288=DIRECTION('ref_axis',(-0.900968867902416,-0.433883739117565,-7.97031498468616E-17));
#17289=DIRECTION('center_axis',(-7.97031498468617E-17,3.49202315903319E-16,
-1.));
#17290=DIRECTION('ref_axis',(0.900968867902416,0.433883739117565,7.97031498468616E-17));
#17291=DIRECTION('center_axis',(7.97031498468617E-17,-3.49202315903319E-16,
1.));
#17292=DIRECTION('ref_axis',(-0.900968867902416,-0.433883739117565,-7.97031498468616E-17));
#17293=DIRECTION('center_axis',(7.97031498468617E-17,-3.49202315903319E-16,
1.));
#17294=DIRECTION('ref_axis',(-0.900968867902416,-0.433883739117565,-7.97031498468616E-17));
#17295=DIRECTION('center_axis',(7.97031498468617E-17,-3.49202315903319E-16,
1.));
#17296=DIRECTION('ref_axis',(-0.900968867902416,-0.433883739117565,-7.97031498468616E-17));
#17297=DIRECTION('center_axis',(7.97031498468617E-17,-3.49202315903319E-16,
1.));
#17298=DIRECTION('ref_axis',(-0.900968867902416,-0.433883739117565,-7.97031498468616E-17));
#17299=DIRECTION('center_axis',(-0.433883739117565,0.900968867902416,3.49202315903319E-16));
#17300=DIRECTION('ref_axis',(-7.97031498468617E-17,3.49202315903319E-16,
-1.));
#17301=DIRECTION('center_axis',(0.433883739117565,-0.900968867902416,-3.49202315903319E-16));
#17302=DIRECTION('ref_axis',(7.97031498468617E-17,-3.49202315903319E-16,
1.));
#17303=DIRECTION('center_axis',(7.97031498468617E-17,-3.49202315903319E-16,
1.));
#17304=DIRECTION('ref_axis',(-0.900968867902416,-0.433883739117565,-7.97031498468616E-17));
#17305=DIRECTION('center_axis',(-7.97031498468617E-17,3.49202315903319E-16,
-1.));
#17306=DIRECTION('ref_axis',(-0.900968867902416,-0.433883739117565,-7.97031498468616E-17));
#17307=DIRECTION('center_axis',(7.97031498468617E-17,-3.49202315903319E-16,
1.));
#17308=DIRECTION('ref_axis',(-0.900968867902416,-0.433883739117565,-7.97031498468616E-17));
#17309=DIRECTION('center_axis',(7.97031498468617E-17,-3.49202315903319E-16,
1.));
#17310=DIRECTION('ref_axis',(-0.900968867902416,-0.433883739117565,-7.97031498468616E-17));
#17311=DIRECTION('center_axis',(-7.97031498468617E-17,3.49202315903319E-16,
-1.));
#17312=DIRECTION('ref_axis',(-0.900968867902416,-0.433883739117565,-7.97031498468616E-17));
#17313=DIRECTION('center_axis',(7.97031498468617E-17,-3.49202315903319E-16,
1.));
#17314=DIRECTION('ref_axis',(-0.900968867902416,-0.433883739117565,-7.97031498468616E-17));
#17315=DIRECTION('center_axis',(-7.97031498468617E-17,3.49202315903319E-16,
-1.));
#17316=DIRECTION('ref_axis',(0.900968867902416,0.433883739117565,7.97031498468616E-17));
#17317=DIRECTION('center_axis',(-7.97031498468617E-17,3.49202315903319E-16,
-1.));
#17318=DIRECTION('ref_axis',(0.900968867902416,0.433883739117565,7.97031498468616E-17));
#17319=DIRECTION('center_axis',(7.97031498468594E-17,3.4920231590332E-16,
-1.));
#17320=DIRECTION('ref_axis',(0.900968867902422,-0.433883739117553,-7.97031498468594E-17));
#17321=DIRECTION('center_axis',(7.97031498468594E-17,3.4920231590332E-16,
-1.));
#17322=DIRECTION('ref_axis',(-0.900968867902422,0.433883739117553,7.97031498468594E-17));
#17323=DIRECTION('center_axis',(7.97031498468594E-17,3.4920231590332E-16,
-1.));
#17324=DIRECTION('ref_axis',(-0.900968867902422,0.433883739117553,7.97031498468594E-17));
#17325=DIRECTION('center_axis',(7.97031498468594E-17,3.4920231590332E-16,
-1.));
#17326=DIRECTION('ref_axis',(0.900968867902422,-0.433883739117553,-7.97031498468594E-17));
#17327=DIRECTION('center_axis',(-7.97031498468594E-17,-3.4920231590332E-16,
1.));
#17328=DIRECTION('ref_axis',(-0.900968867902422,0.433883739117553,7.97031498468594E-17));
#17329=DIRECTION('center_axis',(-7.97031498468594E-17,-3.4920231590332E-16,
1.));
#17330=DIRECTION('ref_axis',(-0.900968867902422,0.433883739117553,7.97031498468594E-17));
#17331=DIRECTION('center_axis',(-7.97031498468594E-17,-3.4920231590332E-16,
1.));
#17332=DIRECTION('ref_axis',(-0.900968867902422,0.433883739117553,7.97031498468594E-17));
#17333=DIRECTION('center_axis',(-7.97031498468594E-17,-3.4920231590332E-16,
1.));
#17334=DIRECTION('ref_axis',(-0.900968867902422,0.433883739117553,7.97031498468594E-17));
#17335=DIRECTION('center_axis',(0.433883739117553,0.900968867902422,3.4920231590332E-16));
#17336=DIRECTION('ref_axis',(7.97031498468594E-17,3.4920231590332E-16,-1.));
#17337=DIRECTION('center_axis',(-0.433883739117553,-0.900968867902422,-3.4920231590332E-16));
#17338=DIRECTION('ref_axis',(-7.97031498468594E-17,-3.4920231590332E-16,
1.));
#17339=DIRECTION('center_axis',(-7.97031498468594E-17,-3.4920231590332E-16,
1.));
#17340=DIRECTION('ref_axis',(-0.900968867902422,0.433883739117553,7.97031498468594E-17));
#17341=DIRECTION('center_axis',(7.97031498468594E-17,3.4920231590332E-16,
-1.));
#17342=DIRECTION('ref_axis',(-0.900968867902422,0.433883739117553,7.97031498468594E-17));
#17343=DIRECTION('center_axis',(-7.97031498468594E-17,-3.4920231590332E-16,
1.));
#17344=DIRECTION('ref_axis',(-0.900968867902422,0.433883739117553,7.97031498468594E-17));
#17345=DIRECTION('center_axis',(-7.97031498468594E-17,-3.4920231590332E-16,
1.));
#17346=DIRECTION('ref_axis',(-0.900968867902422,0.433883739117553,7.97031498468594E-17));
#17347=DIRECTION('center_axis',(7.97031498468594E-17,3.4920231590332E-16,
-1.));
#17348=DIRECTION('ref_axis',(-0.900968867902422,0.433883739117553,7.97031498468594E-17));
#17349=DIRECTION('center_axis',(-7.97031498468594E-17,-3.4920231590332E-16,
1.));
#17350=DIRECTION('ref_axis',(-0.900968867902422,0.433883739117553,7.97031498468594E-17));
#17351=DIRECTION('center_axis',(7.97031498468594E-17,3.4920231590332E-16,
-1.));
#17352=DIRECTION('ref_axis',(0.900968867902422,-0.433883739117553,-7.97031498468594E-17));
#17353=DIRECTION('center_axis',(7.97031498468594E-17,3.4920231590332E-16,
-1.));
#17354=DIRECTION('ref_axis',(0.900968867902422,-0.433883739117553,-7.97031498468594E-17));
#17355=DIRECTION('center_axis',(1.79091352057932E-16,2.24573452299036E-16,
-1.));
#17356=DIRECTION('ref_axis',(0.222520933956318,-0.974927912181823,-1.79091352057933E-16));
#17357=DIRECTION('center_axis',(1.79091352057932E-16,2.24573452299036E-16,
-1.));
#17358=DIRECTION('ref_axis',(-0.222520933956318,0.974927912181823,1.79091352057933E-16));
#17359=DIRECTION('center_axis',(1.79091352057932E-16,2.24573452299036E-16,
-1.));
#17360=DIRECTION('ref_axis',(-0.222520933956318,0.974927912181823,1.79091352057933E-16));
#17361=DIRECTION('center_axis',(1.79091352057932E-16,2.24573452299036E-16,
-1.));
#17362=DIRECTION('ref_axis',(0.222520933956318,-0.974927912181823,-1.79091352057933E-16));
#17363=DIRECTION('center_axis',(-1.79091352057932E-16,-2.24573452299036E-16,
1.));
#17364=DIRECTION('ref_axis',(-0.222520933956318,0.974927912181823,1.79091352057933E-16));
#17365=DIRECTION('center_axis',(-1.79091352057932E-16,-2.24573452299036E-16,
1.));
#17366=DIRECTION('ref_axis',(-0.222520933956318,0.974927912181823,1.79091352057933E-16));
#17367=DIRECTION('center_axis',(-1.79091352057932E-16,-2.24573452299036E-16,
1.));
#17368=DIRECTION('ref_axis',(-0.222520933956318,0.974927912181823,1.79091352057933E-16));
#17369=DIRECTION('center_axis',(-1.79091352057932E-16,-2.24573452299036E-16,
1.));
#17370=DIRECTION('ref_axis',(-0.222520933956318,0.974927912181823,1.79091352057933E-16));
#17371=DIRECTION('center_axis',(0.974927912181823,0.222520933956318,2.24573452299036E-16));
#17372=DIRECTION('ref_axis',(1.79091352057932E-16,2.24573452299036E-16,
-1.));
#17373=DIRECTION('center_axis',(-0.974927912181823,-0.222520933956318,-2.24573452299036E-16));
#17374=DIRECTION('ref_axis',(-1.79091352057932E-16,-2.24573452299036E-16,
1.));
#17375=DIRECTION('center_axis',(-1.79091352057932E-16,-2.24573452299036E-16,
1.));
#17376=DIRECTION('ref_axis',(-0.222520933956318,0.974927912181823,1.79091352057933E-16));
#17377=DIRECTION('center_axis',(1.79091352057932E-16,2.24573452299036E-16,
-1.));
#17378=DIRECTION('ref_axis',(-0.222520933956318,0.974927912181823,1.79091352057933E-16));
#17379=DIRECTION('center_axis',(-1.79091352057932E-16,-2.24573452299036E-16,
1.));
#17380=DIRECTION('ref_axis',(-0.222520933956318,0.974927912181823,1.79091352057933E-16));
#17381=DIRECTION('center_axis',(-1.79091352057932E-16,-2.24573452299036E-16,
1.));
#17382=DIRECTION('ref_axis',(-0.222520933956318,0.974927912181823,1.79091352057933E-16));
#17383=DIRECTION('center_axis',(1.79091352057932E-16,2.24573452299036E-16,
-1.));
#17384=DIRECTION('ref_axis',(-0.222520933956318,0.974927912181823,1.79091352057933E-16));
#17385=DIRECTION('center_axis',(-1.79091352057932E-16,-2.24573452299036E-16,
1.));
#17386=DIRECTION('ref_axis',(-0.222520933956318,0.974927912181823,1.79091352057933E-16));
#17387=DIRECTION('center_axis',(1.79091352057932E-16,2.24573452299036E-16,
-1.));
#17388=DIRECTION('ref_axis',(0.222520933956318,-0.974927912181823,-1.79091352057933E-16));
#17389=DIRECTION('center_axis',(1.79091352057932E-16,2.24573452299036E-16,
-1.));
#17390=DIRECTION('ref_axis',(0.222520933956318,-0.974927912181823,-1.79091352057933E-16));
#17391=DIRECTION('center_axis',(1.43620113371566E-16,6.91638013500059E-17,
-1.));
#17392=DIRECTION('ref_axis',(-0.623489801858732,-0.781831482468031,-1.43620113371566E-16));
#17393=DIRECTION('center_axis',(1.43620113371566E-16,6.91638013500059E-17,
-1.));
#17394=DIRECTION('ref_axis',(0.623489801858732,0.781831482468031,1.43620113371566E-16));
#17395=DIRECTION('center_axis',(1.43620113371566E-16,6.91638013500059E-17,
-1.));
#17396=DIRECTION('ref_axis',(0.623489801858732,0.781831482468031,1.43620113371566E-16));
#17397=DIRECTION('center_axis',(1.43620113371566E-16,6.91638013500059E-17,
-1.));
#17398=DIRECTION('ref_axis',(-0.623489801858732,-0.781831482468031,-1.43620113371566E-16));
#17399=DIRECTION('center_axis',(-1.43620113371566E-16,-6.91638013500059E-17,
1.));
#17400=DIRECTION('ref_axis',(0.623489801858732,0.781831482468031,1.43620113371566E-16));
#17401=DIRECTION('center_axis',(-1.43620113371566E-16,-6.91638013500059E-17,
1.));
#17402=DIRECTION('ref_axis',(0.623489801858732,0.781831482468031,1.43620113371566E-16));
#17403=DIRECTION('center_axis',(-1.43620113371566E-16,-6.91638013500059E-17,
1.));
#17404=DIRECTION('ref_axis',(0.623489801858732,0.781831482468031,1.43620113371566E-16));
#17405=DIRECTION('center_axis',(-1.43620113371566E-16,-6.91638013500059E-17,
1.));
#17406=DIRECTION('ref_axis',(0.623489801858732,0.781831482468031,1.43620113371566E-16));
#17407=DIRECTION('center_axis',(0.781831482468031,-0.623489801858732,6.91638013500059E-17));
#17408=DIRECTION('ref_axis',(1.43620113371566E-16,6.91638013500061E-17,
-1.));
#17409=DIRECTION('center_axis',(-0.781831482468031,0.623489801858732,-6.91638013500059E-17));
#17410=DIRECTION('ref_axis',(-1.43620113371566E-16,-6.91638013500061E-17,
1.));
#17411=DIRECTION('center_axis',(-1.43620113371566E-16,-6.91638013500059E-17,
1.));
#17412=DIRECTION('ref_axis',(0.623489801858732,0.781831482468031,1.43620113371566E-16));
#17413=DIRECTION('center_axis',(1.43620113371566E-16,6.91638013500059E-17,
-1.));
#17414=DIRECTION('ref_axis',(0.623489801858732,0.781831482468031,1.43620113371566E-16));
#17415=DIRECTION('center_axis',(-1.43620113371566E-16,-6.91638013500059E-17,
1.));
#17416=DIRECTION('ref_axis',(0.623489801858732,0.781831482468031,1.43620113371566E-16));
#17417=DIRECTION('center_axis',(-1.43620113371566E-16,-6.91638013500059E-17,
1.));
#17418=DIRECTION('ref_axis',(0.623489801858732,0.781831482468031,1.43620113371566E-16));
#17419=DIRECTION('center_axis',(1.43620113371566E-16,6.91638013500059E-17,
-1.));
#17420=DIRECTION('ref_axis',(0.623489801858732,0.781831482468031,1.43620113371566E-16));
#17421=DIRECTION('center_axis',(-1.43620113371566E-16,-6.91638013500059E-17,
1.));
#17422=DIRECTION('ref_axis',(0.623489801858732,0.781831482468031,1.43620113371566E-16));
#17423=DIRECTION('center_axis',(1.43620113371566E-16,6.91638013500059E-17,
-1.));
#17424=DIRECTION('ref_axis',(-0.623489801858732,-0.781831482468031,-1.43620113371566E-16));
#17425=DIRECTION('center_axis',(1.43620113371566E-16,6.91638013500059E-17,
-1.));
#17426=DIRECTION('ref_axis',(-0.623489801858732,-0.781831482468031,-1.43620113371566E-16));
#17427=DIRECTION('center_axis',(0.,0.,1.));
#17428=DIRECTION('ref_axis',(1.,0.,0.));
#17429=DIRECTION('center_axis',(0.,0.,-1.));
#17430=DIRECTION('ref_axis',(1.,0.,0.));
#17431=DIRECTION('center_axis',(0.,0.,1.));
#17432=DIRECTION('ref_axis',(1.,0.,0.));
#17433=DIRECTION('center_axis',(0.,0.,1.));
#17434=DIRECTION('ref_axis',(1.,0.,0.));
#17435=DIRECTION('center_axis',(0.,0.,-1.));
#17436=DIRECTION('ref_axis',(1.,0.,0.));
#17437=DIRECTION('center_axis',(0.,0.,1.));
#17438=DIRECTION('ref_axis',(1.,0.,0.));
#17439=DIRECTION('center_axis',(0.,0.,-1.));
#17440=DIRECTION('ref_axis',(-1.,0.,0.));
#17441=DIRECTION('center_axis',(0.,0.,-1.));
#17442=DIRECTION('ref_axis',(-1.,0.,0.));
#39437=CARTESIAN_POINT('',(0.,0.,0.));
#39438=CARTESIAN_POINT('Origin',(0.,1.73472347597681E-15,-6.67403582113016E-15));
#39439=CARTESIAN_POINT('',(1.52656933693714E-15,12.4653846153846,3.0875));
#39440=CARTESIAN_POINT('Origin',(0.,6.26866080313552E-16,3.0875));
#39441=CARTESIAN_POINT('',(-1.52656933693714E-15,12.4653846153846,-3.0875));
#39442=CARTESIAN_POINT('Origin',(-1.74512168878498E-15,14.25,-4.05635328795269E-15));
#39443=CARTESIAN_POINT('Origin',(0.,1.76119517802379E-15,-3.0875));
#39444=CARTESIAN_POINT('Origin',(0.,1.56496838953657E-16,5.64807088834312));
#39445=CARTESIAN_POINT('',(9.67029207191279E-16,7.64278544417155,5.99278544417156));
#39446=CARTESIAN_POINT('',(-9.35971273077467E-16,-7.64278544417155,5.99278544417156));
#39447=CARTESIAN_POINT('Origin',(0.,9.31738023414375E-17,5.99278544417156));
#39448=CARTESIAN_POINT('Origin',(0.,9.31738023414375E-17,5.99278544417156));
#39449=CARTESIAN_POINT('',(-9.18485099360515E-16,-7.5,5.64807088834312));
#39450=CARTESIAN_POINT('Origin',(-9.78186630818948E-16,-7.9875,5.64807088834312));
#39451=CARTESIAN_POINT('',(9.18485099360515E-16,7.5,5.64807088834312));
#39452=CARTESIAN_POINT('Origin',(0.,1.56496838953657E-16,5.64807088834312));
#39453=CARTESIAN_POINT('Origin',(0.,1.56496838953657E-16,5.64807088834312));
#39454=CARTESIAN_POINT('Origin',(0.,2.23156441938368E-15,-5.64807088834312));
#39455=CARTESIAN_POINT('',(9.18485099360515E-16,7.5,-5.64807088834312));
#39456=CARTESIAN_POINT('',(-9.18485099360515E-16,-7.5,-5.64807088834312));
#39457=CARTESIAN_POINT('Origin',(0.,2.23156441938368E-15,-5.64807088834312));
#39458=CARTESIAN_POINT('Origin',(0.,2.23156441938368E-15,-5.64807088834312));
#39459=CARTESIAN_POINT('',(-9.35971273077467E-16,-7.64278544417155,-5.99278544417156));
#39460=CARTESIAN_POINT('Origin',(-9.78186630818948E-16,-7.9875,-5.64807088834312));
#39461=CARTESIAN_POINT('Origin',(0.,2.2948874559959E-15,-5.99278544417156));
#39462=CARTESIAN_POINT('Origin',(0.,-9.99635681210842E-31,6.5));
#39463=CARTESIAN_POINT('',(-9.98087141305092E-16,8.14999999999999,6.50000000000001));
#39464=CARTESIAN_POINT('',(-9.98087141305092E-16,8.14999999999999,6.5));
#39465=CARTESIAN_POINT('Origin',(0.,-9.99635681210842E-31,6.5));
#39466=CARTESIAN_POINT('Origin',(0.,0.,6.5));
#39467=CARTESIAN_POINT('',(-9.18485099360515E-16,7.5,6.5));
#39468=CARTESIAN_POINT('Origin',(0.,2.26865819542047E-15,-5.85));
#39469=CARTESIAN_POINT('',(-9.98087141305091E-16,-8.14999999999998,-6.50000000000001));
#39470=CARTESIAN_POINT('',(-9.18485099360515E-16,-7.5,-5.85));
#39471=CARTESIAN_POINT('Origin',(0.,2.38806125833734E-15,-6.50000000000001));
#39472=CARTESIAN_POINT('Origin',(0.,0.,6.5));
#39473=CARTESIAN_POINT('',(-1.52656933693714E-15,12.4653846153846,-6.50000000000001));
#39474=CARTESIAN_POINT('',(-1.52656933693714E-15,12.4653846153846,6.5));
#39475=CARTESIAN_POINT('Origin',(0.,2.38806125833734E-15,-6.50000000000001));
#39476=CARTESIAN_POINT('Origin',(0.,0.,6.5));
#39477=CARTESIAN_POINT('',(-1.52656933693714E-15,12.4653846153846,6.50000000000001));
#39478=CARTESIAN_POINT('Origin',(0.,-1.17267830746035E-30,6.50000000000001));
#39479=CARTESIAN_POINT('',(-1.52656933693714E-15,12.4653846153846,6.5));
#39480=CARTESIAN_POINT('Origin',(0.,8.14999999999999,6.50000000000001));
#39481=CARTESIAN_POINT('Origin',(0.,8.14999999999999,-6.50000000000001));
#39482=CARTESIAN_POINT('Origin',(0.,14.25,-4.07195060716495E-15));
#39483=CARTESIAN_POINT('',(-3.56616156686793,14.25,-4.07195060716495E-15));
#39484=CARTESIAN_POINT('',(3.56616156686793,14.25,-4.07195060716495E-15));
#39485=CARTESIAN_POINT('Origin',(0.,14.25,-4.07195060716495E-15));
#39486=CARTESIAN_POINT('Origin',(11.1410986251694,8.88472967648693,-5.05753477640253E-15));
#39487=CARTESIAN_POINT('',(8.91763325644669,11.6728670610318,-4.54536224786764E-15));
#39488=CARTESIAN_POINT('',(13.3645639938921,6.09659229194206,-5.56970730493742E-15));
#39489=CARTESIAN_POINT('Origin',(11.1410986251694,8.88472967648693,-5.05753477640253E-15));
#39490=CARTESIAN_POINT('Origin',(13.892722748591,-3.17092330887753,-7.27212230242621E-15));
#39491=CARTESIAN_POINT('',(14.6862683510896,0.305827142012077,-6.6334536057588E-15));
#39492=CARTESIAN_POINT('',(13.0991771460924,-6.64767375976714,-7.91079099909362E-15));
#39493=CARTESIAN_POINT('Origin',(13.892722748591,-3.17092330887753,-7.27212230242621E-15));
#39494=CARTESIAN_POINT('Origin',(6.18284328242512,-12.8388063676095,-9.04808360878726E-15));
#39495=CARTESIAN_POINT('',(9.39584383208325,-11.2915068526795,-8.76384929904507E-15));
#39496=CARTESIAN_POINT('',(2.96984273276699,-14.3861058825395,-9.33231791852945E-15));
#39497=CARTESIAN_POINT('Origin',(6.18284328242512,-12.8388063676095,-9.04808360878726E-15));
#39498=CARTESIAN_POINT('Origin',(-6.1828432824253,-12.8388063676094,-9.04808360878725E-15));
#39499=CARTESIAN_POINT('',(-2.9698427327672,-14.3861058825394,-9.33231791852944E-15));
#39500=CARTESIAN_POINT('',(-9.39584383208341,-11.2915068526794,-8.76384929904506E-15));
#39501=CARTESIAN_POINT('Origin',(-6.1828432824253,-12.8388063676094,-9.04808360878725E-15));
#39502=CARTESIAN_POINT('Origin',(-13.892722748591,-3.17092330887735,-7.27212230242617E-15));
#39503=CARTESIAN_POINT('',(-13.0991771460925,-6.64767375976697,-7.91079099909359E-15));
#39504=CARTESIAN_POINT('',(-14.6862683510895,0.30582714201227,-6.63345360575876E-15));
#39505=CARTESIAN_POINT('Origin',(-13.892722748591,-3.17092330887735,-7.27212230242617E-15));
#39506=CARTESIAN_POINT('Origin',(-11.1410986251693,8.88472967648709,-5.0575347764025E-15));
#39507=CARTESIAN_POINT('',(-13.3645639938921,6.09659229194225,-5.56970730493739E-15));
#39508=CARTESIAN_POINT('',(-8.91763325644655,11.6728670610319,-4.54536224786761E-15));
#39509=CARTESIAN_POINT('Origin',(-11.1410986251693,8.88472967648709,-5.0575347764025E-15));
#39510=CARTESIAN_POINT('Origin',(0.,1.07462756625201E-17,6.44149999999999));
#39511=CARTESIAN_POINT('',(-1.99949495950787E-15,-16.3271153846154,6.49999999999999));
#39512=CARTESIAN_POINT('Origin',(0.,2.01169401222323E-30,6.49999999999999));
#39513=CARTESIAN_POINT('',(-1.99233077573286E-15,-16.2686153846154,6.44149999999999));
#39514=CARTESIAN_POINT('Origin',(-1.99949495950788E-15,-16.3271153846154,
6.44149999999999));
#39515=CARTESIAN_POINT('',(1.99233077573286E-15,16.2686153846154,6.44149999999999));
#39516=CARTESIAN_POINT('Origin',(0.,1.07462756625199E-17,6.44149999999999));
#39517=CARTESIAN_POINT('Origin',(0.,1.07462756625199E-17,6.44149999999999));
#39518=CARTESIAN_POINT('Origin',(0.,1.30149338579385E-16,5.7915));
#39519=CARTESIAN_POINT('',(-1.96367404063281E-15,16.0346153846154,5.7915));
#39520=CARTESIAN_POINT('Origin',(0.,1.30149338579385E-16,5.7915));
#39521=CARTESIAN_POINT('',(-1.97083822440782E-15,16.0931153846154,5.85));
#39522=CARTESIAN_POINT('Origin',(-1.97083822440783E-15,16.0931153846154,
5.7915));
#39523=CARTESIAN_POINT('Origin',(0.,1.19403062916867E-16,5.85));
#39524=CARTESIAN_POINT('Origin',(0.,2.37731498267482E-15,-6.44150000000001));
#39525=CARTESIAN_POINT('',(-1.99949495950787E-15,16.3271153846154,-6.5));
#39526=CARTESIAN_POINT('Origin',(0.,2.38806125833734E-15,-6.50000000000001));
#39527=CARTESIAN_POINT('',(-1.99233077573286E-15,16.2686153846154,-6.4415));
#39528=CARTESIAN_POINT('Origin',(-1.99949495950788E-15,16.3271153846154,
-6.44150000000001));
#39529=CARTESIAN_POINT('Origin',(0.,2.37731498267482E-15,-6.44150000000001));
#39530=CARTESIAN_POINT('Origin',(0.,2.25791191975795E-15,-5.7915));
#39531=CARTESIAN_POINT('',(1.96367404063281E-15,16.0346153846154,-5.7915));
#39532=CARTESIAN_POINT('',(-1.96367404063282E-15,-16.0346153846154,-5.7915));
#39533=CARTESIAN_POINT('Origin',(0.,2.25791191975795E-15,-5.7915));
#39534=CARTESIAN_POINT('Origin',(0.,2.25791191975795E-15,-5.7915));
#39535=CARTESIAN_POINT('',(-1.97083822440782E-15,-16.0931153846154,-5.85000000000001));
#39536=CARTESIAN_POINT('Origin',(-1.97083822440783E-15,-16.0931153846154,
-5.7915));
#39537=CARTESIAN_POINT('Origin',(0.,2.26865819542047E-15,-5.85));
#39538=CARTESIAN_POINT('Origin',(0.,0.,6.5));
#39539=CARTESIAN_POINT('',(-2.16636878649169E-15,17.6897435897436,5.85));
#39540=CARTESIAN_POINT('Origin',(0.,1.19403062916867E-16,5.85));
#39541=CARTESIAN_POINT('',(-2.16636878649169E-15,17.6897435897436,6.084));
#39542=CARTESIAN_POINT('',(-2.16636878649169E-15,17.6897435897436,6.5));
#39543=CARTESIAN_POINT('Origin',(0.,7.6417960266795E-17,6.084));
#39544=CARTESIAN_POINT('Origin',(0.,0.,6.5));
#39545=CARTESIAN_POINT('',(-1.99233077573286E-15,16.2686153846154,6.084));
#39546=CARTESIAN_POINT('Origin',(0.,7.6417960266795E-17,6.084));
#39547=CARTESIAN_POINT('',(-1.99233077573286E-15,16.2686153846154,6.5));
#39548=CARTESIAN_POINT('Origin',(0.,0.,6.5));
#39549=CARTESIAN_POINT('',(-1.96367404063281E-15,16.0346153846154,-3.0875));
#39550=CARTESIAN_POINT('',(-1.96367404063282E-15,16.0346153846154,6.5));
#39551=CARTESIAN_POINT('Origin',(0.,1.76119517802379E-15,-3.08750000000001));
#39552=CARTESIAN_POINT('Origin',(0.,1.73472347597681E-15,-6.67403582113016E-15));
#39553=CARTESIAN_POINT('',(-1.96367404063281E-15,16.0346153846154,3.0875));
#39554=CARTESIAN_POINT('Origin',(-1.74512168878498E-15,14.25,-4.05635328795269E-15));
#39555=CARTESIAN_POINT('Origin',(0.,6.26866080313552E-16,3.08749999999999));
#39556=CARTESIAN_POINT('Origin',(0.,0.,6.5));
#39557=CARTESIAN_POINT('',(-1.96367404063282E-15,16.0346153846154,6.5));
#39558=CARTESIAN_POINT('Origin',(0.,0.,6.5));
#39559=CARTESIAN_POINT('',(-1.99233077573286E-15,16.2686153846154,-6.084));
#39560=CARTESIAN_POINT('',(-1.99233077573286E-15,16.2686153846154,6.5));
#39561=CARTESIAN_POINT('Origin',(0.,2.31164329807054E-15,-6.084));
#39562=CARTESIAN_POINT('Origin',(0.,0.,6.5));
#39563=CARTESIAN_POINT('',(-2.16636878649169E-15,17.6897435897436,-6.084));
#39564=CARTESIAN_POINT('Origin',(0.,2.31164329807054E-15,-6.084));
#39565=CARTESIAN_POINT('',(-2.16636878649169E-15,17.6897435897436,-5.85));
#39566=CARTESIAN_POINT('',(-2.16636878649169E-15,17.6897435897436,6.5));
#39567=CARTESIAN_POINT('Origin',(0.,2.26865819542047E-15,-5.85));
#39568=CARTESIAN_POINT('Origin',(0.,2.38806125833734E-15,-6.50000000000001));
#39569=CARTESIAN_POINT('',(-2.57175827820944E-15,21.,-5.85));
#39570=CARTESIAN_POINT('Origin',(0.,2.26865819542047E-15,-5.85000000000001));
#39571=CARTESIAN_POINT('',(-2.49215623626487E-15,20.35,-6.5));
#39572=CARTESIAN_POINT('',(-2.49215623626486E-15,20.35,-6.50000000000001));
#39573=CARTESIAN_POINT('Origin',(0.,2.38806125833734E-15,-6.50000000000001));
#39574=CARTESIAN_POINT('Origin',(0.,1.19403062916869E-16,5.84999999999999));
#39575=CARTESIAN_POINT('',(2.57175827820944E-15,21.,5.84999999999999));
#39576=CARTESIAN_POINT('',(-2.57175827820944E-15,-21.,5.84999999999999));
#39577=CARTESIAN_POINT('Origin',(0.,1.19403062916869E-16,5.84999999999999));
#39578=CARTESIAN_POINT('',(-2.49215623626487E-15,-20.35,6.49999999999999));
#39579=CARTESIAN_POINT('',(-2.57175827820944E-15,-21.,5.84999999999999));
#39580=CARTESIAN_POINT('Origin',(0.,1.96135664184276E-30,6.49999999999999));
#39581=CARTESIAN_POINT('Origin',(0.,1.19403062916869E-16,5.84999999999999));
#39582=CARTESIAN_POINT('Origin',(0.,0.,6.5));
#39583=CARTESIAN_POINT('',(-2.57175827820944E-15,21.,6.5));
#39584=CARTESIAN_POINT('Origin',(0.,20.35,6.49999999999999));
#39585=CARTESIAN_POINT('Origin',(0.,20.35,-6.5));
#39586=CARTESIAN_POINT('Origin',(0.,16.0346153846154,-5.85));
#39587=CARTESIAN_POINT('Origin',(0.,16.2686153846154,-6.084));
#39588=CARTESIAN_POINT('Origin',(0.,16.2686153846154,6.084));
#39589=CARTESIAN_POINT('Origin',(0.,16.0346153846154,5.85));
#39590=CARTESIAN_POINT('Origin',(-11.1410986251694,8.88472967648693,-9.85584169237584E-16));
#39591=CARTESIAN_POINT('',(-11.838732871064,9.44107442276088,-3.96060240207311));
#39592=CARTESIAN_POINT('Origin',(-11.838732871064,9.44107442276088,-1.04729956121144E-15));
#39593=CARTESIAN_POINT('',(-10.4434643792749,8.32838493021299,-3.96060240207311));
#39594=CARTESIAN_POINT('Origin',(-11.1410986251694,8.88472967648693,-2.5198520116158));
#39595=CARTESIAN_POINT('Origin',(-10.4434643792749,8.32838493021299,-9.23868777263733E-16));
#39596=CARTESIAN_POINT('',(-13.176267261227,5.42664547033602,1.08333333333333));
#39597=CARTESIAN_POINT('',(-13.9269936544441,5.94376395877182,1.08333333333333));
#39598=CARTESIAN_POINT('Ctrl Pts',(-13.176267261227,5.42664547033603,1.08333333333333));
#39599=CARTESIAN_POINT('Ctrl Pts',(-13.3544742809805,5.48608062863209,1.08333333333333));
#39600=CARTESIAN_POINT('Ctrl Pts',(-13.5395781511317,5.58798093945111,1.08333333333333));
#39601=CARTESIAN_POINT('Ctrl Pts',(-13.7657237213497,5.76832601371359,1.08333333333333));
#39602=CARTESIAN_POINT('Ctrl Pts',(-13.851789663848,5.85187873682469,1.08333333333333));
#39603=CARTESIAN_POINT('Ctrl Pts',(-13.9269936544446,5.9437639587714,1.08333333333333));
#39604=CARTESIAN_POINT('',(-13.176267261227,5.42664547033602,-1.08333333333333));
#39605=CARTESIAN_POINT('Ctrl Pts',(-13.176267261227,5.426645470336,1.08333333333333));
#39606=CARTESIAN_POINT('Ctrl Pts',(-13.1893705593041,5.39482976422217,0.949270311030458));
#39607=CARTESIAN_POINT('Ctrl Pts',(-13.1999097963793,5.36892368585873,0.813521288367943));
#39608=CARTESIAN_POINT('Ctrl Pts',(-13.2079621630869,5.34904061477063,0.676607052100963));
#39609=CARTESIAN_POINT('Ctrl Pts',(-13.2148460430323,5.33204279546006,0.559560573777783));
#39610=CARTESIAN_POINT('Ctrl Pts',(-13.2199117356377,5.31944645364942,0.441662516279014));
#39611=CARTESIAN_POINT('Ctrl Pts',(-13.2231796369648,5.31131059989529,0.323238258334693));
#39612=CARTESIAN_POINT('Ctrl Pts',(-13.2269557156994,5.30190957419894,0.186398348762648));
#39613=CARTESIAN_POINT('Ctrl Pts',(-13.2283213471704,5.29849241313602,0.0492519096262365));
#39614=CARTESIAN_POINT('Ctrl Pts',(-13.2273014856384,5.30103720115478,-0.0876758270660023));
#39615=CARTESIAN_POINT('Ctrl Pts',(-13.2262786675027,5.30358936657696,-0.225000520654269));
#39616=CARTESIAN_POINT('Ctrl Pts',(-13.2228564747501,5.31213809759637,-0.362105241912721));
#39617=CARTESIAN_POINT('Ctrl Pts',(-13.21701132539,5.32664168351063,-0.498460177595569));
#39618=CARTESIAN_POINT('Ctrl Pts',(-13.2111409592134,5.34120783998416,-0.635403368116636));
#39619=CARTESIAN_POINT('Ctrl Pts',(-13.2028266475275,5.36178038996277,-0.771590289741212));
#39620=CARTESIAN_POINT('Ctrl Pts',(-13.1919958930595,5.38829698119001,-0.90648424252654));
#39621=CARTESIAN_POINT('Ctrl Pts',(-13.1872415508606,5.39993688577963,-0.965698216399817));
#39622=CARTESIAN_POINT('Ctrl Pts',(-13.1820016856382,5.4127218947045,-1.02466304565395));
#39623=CARTESIAN_POINT('Ctrl Pts',(-13.176267261227,5.426645470336,-1.08333333333333));
#39624=CARTESIAN_POINT('',(-13.9269936544455,5.94376395877242,-1.08333333333333));
#39625=CARTESIAN_POINT('Ctrl Pts',(-13.176267261227,5.42664547033603,-1.08333333333333));
#39626=CARTESIAN_POINT('Ctrl Pts',(-13.3544742809805,5.48608062863209,-1.08333333333333));
#39627=CARTESIAN_POINT('Ctrl Pts',(-13.5395781511317,5.58798093945111,-1.08333333333333));
#39628=CARTESIAN_POINT('Ctrl Pts',(-13.76572372135,5.76832601371385,-1.08333333333333));
#39629=CARTESIAN_POINT('Ctrl Pts',(-13.8517896638487,5.85187873682532,-1.08333333333333));
#39630=CARTESIAN_POINT('Ctrl Pts',(-13.9269936544455,5.94376395877245,-1.08333333333333));
#39631=CARTESIAN_POINT('Ctrl Pts',(-13.9269936544444,5.94376395877114,-1.08333333333355));
#39632=CARTESIAN_POINT('Ctrl Pts',(-13.9416885168396,5.90933203032471,-0.95688863210348));
#39633=CARTESIAN_POINT('Ctrl Pts',(-13.9536527109306,5.88095561854246,-0.828820583351296));
#39634=CARTESIAN_POINT('Ctrl Pts',(-13.9629765258054,5.85873440158612,-0.699646919261824));
#39635=CARTESIAN_POINT('Ctrl Pts',(-13.9722513158078,5.83663002439321,-0.571152453813156));
#39636=CARTESIAN_POINT('Ctrl Pts',(-13.9789135007646,5.82061622745832,-0.441563969171476));
#39637=CARTESIAN_POINT('Ctrl Pts',(-13.9830050237945,5.81077040959789,-0.311391073637591));
#39638=CARTESIAN_POINT('Ctrl Pts',(-13.9870637119681,5.80100360534983,-0.182262827807202));
#39639=CARTESIAN_POINT('Ctrl Pts',(-13.9885928700523,5.79730615639837,-0.0525595133518154));
#39640=CARTESIAN_POINT('Ctrl Pts',(-13.9875862925321,5.79973378332902,0.0772214321948836));
#39641=CARTESIAN_POINT('Ctrl Pts',(-13.9868997670034,5.80138952054624,0.16573715053464));
#39642=CARTESIAN_POINT('Ctrl Pts',(-13.9850326975558,5.80589410253377,0.25428898113034));
#39643=CARTESIAN_POINT('Ctrl Pts',(-13.9819702480149,5.81325986277477,0.342719102199523));
#39644=CARTESIAN_POINT('Ctrl Pts',(-13.9773533484511,5.82436436418404,0.476034927301742));
#39645=CARTESIAN_POINT('Ctrl Pts',(-13.9700489046451,5.84190742581559,0.608312350205735));
#39646=CARTESIAN_POINT('Ctrl Pts',(-13.9600480872369,5.86570879353503,0.739057191237609));
#39647=CARTESIAN_POINT('Ctrl Pts',(-13.9511688384278,5.8868408927778,0.855139299994326));
#39648=CARTESIAN_POINT('Ctrl Pts',(-13.9401632237806,5.9129059856334,0.970013302477931));
#39649=CARTESIAN_POINT('Ctrl Pts',(-13.9269936544444,5.94376395877114,1.08333333333355));
#39650=CARTESIAN_POINT('',(-8.89378902201695,12.2552029391753,1.08333333333333));
#39651=CARTESIAN_POINT('',(-8.22258343557141,11.6383685130291,1.08333333333333));
#39652=CARTESIAN_POINT('Ctrl Pts',(-8.89378902201693,12.2552029391753,1.08333333333333));
#39653=CARTESIAN_POINT('Ctrl Pts',(-8.78747309219938,12.2023308550396,1.08333333333333));
#39654=CARTESIAN_POINT('Ctrl Pts',(-8.68686373639314,12.1370149953911,1.08333333333333));
#39655=CARTESIAN_POINT('Ctrl Pts',(-8.46071816617524,11.9566699211287,1.08333333333333));
#39656=CARTESIAN_POINT('Ctrl Pts',(-8.32018322283281,11.7988819437994,1.08333333333333));
#39657=CARTESIAN_POINT('Ctrl Pts',(-8.22258343557192,11.6383685130288,1.08333333333333));
#39658=CARTESIAN_POINT('',(-8.89378902201695,12.2552029391753,-1.08333333333333));
#39659=CARTESIAN_POINT('Ctrl Pts',(-8.89378902201696,12.2552029391753,1.08333333333333));
#39660=CARTESIAN_POINT('Ctrl Pts',(-8.86325700199161,12.2773604951023,0.955915065626613));
#39661=CARTESIAN_POINT('Ctrl Pts',(-8.83806624000395,12.2954729083691,0.8267015714506));
#39662=CARTESIAN_POINT('Ctrl Pts',(-8.81837639229442,12.3095783864577,0.696211209492237));
#39663=CARTESIAN_POINT('Ctrl Pts',(-8.79899689851553,12.3234615321731,0.567777653525536));
#39664=CARTESIAN_POINT('Ctrl Pts',(-8.7849462329058,12.3334631509294,0.438107164856251));
#39665=CARTESIAN_POINT('Ctrl Pts',(-8.77634666705863,12.3395794672318,0.307693975181527));
#39666=CARTESIAN_POINT('Ctrl Pts',(-8.76960830208466,12.3443720314467,0.205506064179221));
#39667=CARTESIAN_POINT('Ctrl Pts',(-8.76621624622179,12.3467783236356,0.102862147741002));
#39668=CARTESIAN_POINT('Ctrl Pts',(-8.76621624622179,12.3467783236356,-2.44249065417534E-15));
#39669=CARTESIAN_POINT('Ctrl Pts',(-8.76621624622179,12.3467783236356,-0.130666807305558));
#39670=CARTESIAN_POINT('Ctrl Pts',(-8.77169236507929,12.3428956683044,-0.261069786498707));
#39671=CARTESIAN_POINT('Ctrl Pts',(-8.78256611126601,12.3351536167882,-0.390710450871087));
#39672=CARTESIAN_POINT('Ctrl Pts',(-8.79357042167237,12.3273186042172,-0.521907748246256));
#39673=CARTESIAN_POINT('Ctrl Pts',(-8.8101027782242,12.315530900308,-0.652324314224256));
#39674=CARTESIAN_POINT('Ctrl Pts',(-8.83205039902736,12.2997710546807,-0.781443489202971));
#39675=CARTESIAN_POINT('Ctrl Pts',(-8.84930597782606,12.2873804060307,-0.882959098491573));
#39676=CARTESIAN_POINT('Ctrl Pts',(-8.86990830867396,12.2725335396739,-0.983672743459536));
#39677=CARTESIAN_POINT('Ctrl Pts',(-8.89378902201696,12.2552029391753,-1.08333333333333));
#39678=CARTESIAN_POINT('',(-8.22258343557665,11.6383685130365,-1.08333333333333));
#39679=CARTESIAN_POINT('Ctrl Pts',(-8.89378902201693,12.2552029391753,-1.08333333333333));
#39680=CARTESIAN_POINT('Ctrl Pts',(-8.78747309219938,12.2023308550396,-1.08333333333333));
#39681=CARTESIAN_POINT('Ctrl Pts',(-8.68686373639314,12.1370149953911,-1.08333333333333));
#39682=CARTESIAN_POINT('Ctrl Pts',(-8.46071816617751,11.9566699211305,-1.08333333333333));
#39683=CARTESIAN_POINT('Ctrl Pts',(-8.32018322283717,11.7988819438045,-1.08333333333333));
#39684=CARTESIAN_POINT('Ctrl Pts',(-8.22258343557662,11.6383685130365,-1.08333333333333));
#39685=CARTESIAN_POINT('Ctrl Pts',(-8.22258343557191,11.6383685130287,-1.08333333333318));
#39686=CARTESIAN_POINT('Ctrl Pts',(-8.19455490688727,11.6581708517696,-0.949622058007629));
#39687=CARTESIAN_POINT('Ctrl Pts',(-8.17172113698899,11.6741565633286,-0.814376693553349));
#39688=CARTESIAN_POINT('Ctrl Pts',(-8.15417398891324,11.6864000683928,-0.678132403728345));
#39689=CARTESIAN_POINT('Ctrl Pts',(-8.13671023659264,11.698585384152,-0.542535637671064));
#39690=CARTESIAN_POINT('Ctrl Pts',(-8.12448291951145,11.7070640382822,-0.405949418799179));
#39691=CARTESIAN_POINT('Ctrl Pts',(-8.11755242812626,11.7118675955896,-0.268901316712111));
#39692=CARTESIAN_POINT('Ctrl Pts',(-8.11302715126356,11.7150040870061,-0.179415511018989));
#39693=CARTESIAN_POINT('Ctrl Pts',(-8.11075954642953,11.7165728598427,-0.0897327832367744));
#39694=CARTESIAN_POINT('Ctrl Pts',(-8.11075954642953,11.7165728598427,-9.99200722162641E-15));
#39695=CARTESIAN_POINT('Ctrl Pts',(-8.11075954642954,11.7165728598427,0.137573936980354));
#39696=CARTESIAN_POINT('Ctrl Pts',(-8.11609005089583,11.7128881555246,0.274951212619692));
#39697=CARTESIAN_POINT('Ctrl Pts',(-8.12669452775723,11.7055258768037,0.4116124062147));
#39698=CARTESIAN_POINT('Ctrl Pts',(-8.13738105388554,11.6981066344457,0.549330978772881));
#39699=CARTESIAN_POINT('Ctrl Pts',(-8.15342350530942,11.6869526399855,0.686322345437031));
#39700=CARTESIAN_POINT('Ctrl Pts',(-8.17473347641523,11.6720277839618,0.822054935347404));
#39701=CARTESIAN_POINT('Ctrl Pts',(-8.18849695174643,11.662388264195,0.909720570537357));
#39702=CARTESIAN_POINT('Ctrl Pts',(-8.20445714658991,11.6511748546878,0.996861109122827));
#39703=CARTESIAN_POINT('Ctrl Pts',(-8.22258343557191,11.6383685130287,1.08333333333318));
#39704=CARTESIAN_POINT('Origin',(-11.1410986251694,8.88472967648693,-9.85584169237584E-16));
#39705=CARTESIAN_POINT('',(-13.6377879061429,6.58029051604744,-1.08333333333333));
#39706=CARTESIAN_POINT('',(-13.2594869773434,6.22835470309403,-1.08333333333333));
#39707=CARTESIAN_POINT('Origin',(-11.1410986251694,8.88472967648693,-1.08333333333333));
#39708=CARTESIAN_POINT('',(-9.02271027299537,11.5411046498798,-1.08333333333333));
#39709=CARTESIAN_POINT('Origin',(-11.1410986251694,8.88472967648693,-9.85584169237584E-16));
#39710=CARTESIAN_POINT('',(-9.45000219633307,11.8316076987796,-1.08333333333333));
#39711=CARTESIAN_POINT('Origin',(-11.1410986251694,8.88472967648693,-1.08333333333333));
#39712=CARTESIAN_POINT('',(-9.45000219633307,11.8316076987796,1.08333333333333));
#39713=CARTESIAN_POINT('Ctrl Pts',(-9.45000219633306,11.8316076987796,-1.08333333333334));
#39714=CARTESIAN_POINT('Ctrl Pts',(-9.35474240837113,11.9076924734257,-0.727666221822799));
#39715=CARTESIAN_POINT('Ctrl Pts',(-9.30796390402501,11.9436715548398,-0.352782973842778));
#39716=CARTESIAN_POINT('Ctrl Pts',(-9.30796390402501,11.9436715548398,-5.10741104345864E-16));
#39717=CARTESIAN_POINT('Ctrl Pts',(-9.30796390402501,11.9436715548398,0.352782973842777));
#39718=CARTESIAN_POINT('Ctrl Pts',(-9.35474240837113,11.9076924734257,0.727666221822798));
#39719=CARTESIAN_POINT('Ctrl Pts',(-9.45000219633306,11.8316076987796,1.08333333333334));
#39720=CARTESIAN_POINT('',(-8.72113759169224,11.2696166353063,1.08333333333333));
#39721=CARTESIAN_POINT('Origin',(-11.1410986251694,8.88472967648693,1.08333333333333));
#39722=CARTESIAN_POINT('',(-8.72113759169224,11.2696166353063,-1.08333333333333));
#39723=CARTESIAN_POINT('Ctrl Pts',(-8.72113759169222,11.2696166353063,1.08333333333334));
#39724=CARTESIAN_POINT('Ctrl Pts',(-8.63036626326988,11.3398611937656,0.725928647976584));
#39725=CARTESIAN_POINT('Ctrl Pts',(-8.58623309669495,11.3727349924818,0.352039859176991));
#39726=CARTESIAN_POINT('Ctrl Pts',(-8.58623309669495,11.3727349924818,-4.46574186955748E-16));
#39727=CARTESIAN_POINT('Ctrl Pts',(-8.58623309669495,11.3727349924818,-0.352039859176992));
#39728=CARTESIAN_POINT('Ctrl Pts',(-8.63036626326988,11.3398611937656,-0.725928647976585));
#39729=CARTESIAN_POINT('Ctrl Pts',(-8.72113759169222,11.2696166353063,-1.08333333333334));
#39730=CARTESIAN_POINT('Origin',(-11.1410986251694,8.88472967648693,-1.08333333333333));
#39731=CARTESIAN_POINT('',(-12.9276994994136,5.99475484510091,-1.08333333333333));
#39732=CARTESIAN_POINT('Origin',(-11.1410986251694,8.88472967648693,-1.08333333333333));
#39733=CARTESIAN_POINT('',(-12.9276994994136,5.99475484510091,1.08333333333333));
#39734=CARTESIAN_POINT('Ctrl Pts',(-12.9276994994136,5.99475484510092,-1.08333333333333));
#39735=CARTESIAN_POINT('Ctrl Pts',(-12.9759843593574,5.89062845864246,-0.725928647976576));
#39736=CARTESIAN_POINT('Ctrl Pts',(-12.9982133898606,5.84028669430256,-0.352039859176989));
#39737=CARTESIAN_POINT('Ctrl Pts',(-12.9982133898606,5.84028669430256,0.352039859176986));
#39738=CARTESIAN_POINT('Ctrl Pts',(-12.9759843593574,5.89062845864246,0.725928647976574));
#39739=CARTESIAN_POINT('Ctrl Pts',(-12.9276994994136,5.99475484510092,1.08333333333332));
#39740=CARTESIAN_POINT('',(-13.6377879061429,6.58029051604744,1.08333333333333));
#39741=CARTESIAN_POINT('Origin',(-11.1410986251694,8.88472967648693,1.08333333333333));
#39742=CARTESIAN_POINT('Ctrl Pts',(-13.6377879061429,6.58029051604746,1.08333333333332));
#39743=CARTESIAN_POINT('Ctrl Pts',(-13.6907677796516,6.47048863474076,0.727666221822783));
#39744=CARTESIAN_POINT('Ctrl Pts',(-13.7154355939007,6.41687686636447,0.352782973842769));
#39745=CARTESIAN_POINT('Ctrl Pts',(-13.7154355939007,6.41687686636447,-0.352782973842771));
#39746=CARTESIAN_POINT('Ctrl Pts',(-13.6907677796516,6.47048863474076,-0.727666221822784));
#39747=CARTESIAN_POINT('Ctrl Pts',(-13.6377879061429,6.58029051604746,-1.08333333333332));
#39748=CARTESIAN_POINT('',(-10.4434643792749,8.32838493021299,3.45272288248773));
#39749=CARTESIAN_POINT('Origin',(-10.4434643792749,8.32838493021299,-9.23868777263733E-16));
#39750=CARTESIAN_POINT('',(-11.838732871064,9.44107442276088,3.45272288248773));
#39751=CARTESIAN_POINT('Origin',(-11.838732871064,9.44107442276088,-1.04729956121144E-15));
#39752=CARTESIAN_POINT('Origin',(-13.892722748591,-3.17092330887753,-3.20017169526126E-15));
#39753=CARTESIAN_POINT('',(-14.7626584240763,-3.36948044994625,-3.96060240207311));
#39754=CARTESIAN_POINT('Origin',(-14.7626584240763,-3.36948044994625,-3.40056031423578E-15));
#39755=CARTESIAN_POINT('',(-13.0227870731057,-2.97236616780882,-3.96060240207311));
#39756=CARTESIAN_POINT('Origin',(-13.892722748591,-3.17092330887753,-2.5198520116158));
#39757=CARTESIAN_POINT('Origin',(-13.0227870731057,-2.97236616780882,-2.99978307628674E-15));
#39758=CARTESIAN_POINT('',(-12.4579905368413,-6.91816245718267,1.08333333333333));
#39759=CARTESIAN_POINT('',(-13.3303603014234,-7.18268588222789,1.08333333333333));
#39760=CARTESIAN_POINT('Ctrl Pts',(-12.4579905368413,-6.91816245718265,
1.08333333333333));
#39761=CARTESIAN_POINT('Ctrl Pts',(-12.6155690741986,-7.02043310055334,
1.08333333333333));
#39762=CARTESIAN_POINT('Ctrl Pts',(-12.8106483205941,-7.10161932916232,
1.08333333333333));
#39763=CARTESIAN_POINT('Ctrl Pts',(-13.0926472341269,-7.16598374096129,
1.08333333333333));
#39764=CARTESIAN_POINT('Ctrl Pts',(-13.211632620936,-7.18117853359748,1.08333333333333));
#39765=CARTESIAN_POINT('Ctrl Pts',(-13.3303603014234,-7.18268588222786,
1.08333333333333));
#39766=CARTESIAN_POINT('',(-12.4579905368413,-6.91816245718267,-1.08333333333334));
#39767=CARTESIAN_POINT('Ctrl Pts',(-12.4579905368413,-6.91816245718269,
1.08333333333333));
#39768=CARTESIAN_POINT('Ctrl Pts',(-12.4412857888864,-6.94824379644449,
0.949270311030495));
#39769=CARTESIAN_POINT('Ctrl Pts',(-12.4276027080703,-6.97263587945683,
0.813521288368019));
#39770=CARTESIAN_POINT('Ctrl Pts',(-12.4170780656485,-6.99132836531023,
0.676607052101084));
#39771=CARTESIAN_POINT('Ctrl Pts',(-12.4080806643214,-7.0073083663671,0.559560573777871));
#39772=CARTESIAN_POINT('Ctrl Pts',(-12.4013908554087,-7.01912257498617,
0.441662516279072));
#39773=CARTESIAN_POINT('Ctrl Pts',(-12.3970674919579,-7.02675014497037,
0.323238258334728));
#39774=CARTESIAN_POINT('Ctrl Pts',(-12.392071820683,-7.03556384585404,0.186398348762656));
#39775=CARTESIAN_POINT('Ctrl Pts',(-12.3902516338786,-7.03876210460556,
0.0492519096262199));
#39776=CARTESIAN_POINT('Ctrl Pts',(-12.3916053560034,-7.03637809537454,
-0.0876758270660418));
#39777=CARTESIAN_POINT('Ctrl Pts',(-12.3929630026022,-7.03398717484178,
-0.22500052065431));
#39778=CARTESIAN_POINT('Ctrl Pts',(-12.3975129673671,-7.02598155019929,
-0.36210524191276));
#39779=CARTESIAN_POINT('Ctrl Pts',(-12.4052079364271,-7.0123687905019,-0.498460177595606));
#39780=CARTESIAN_POINT('Ctrl Pts',(-12.4129361026924,-6.99869730339788,
-0.635403368116707));
#39781=CARTESIAN_POINT('Ctrl Pts',(-12.4238364813948,-6.97937013765694,
-0.771590289741313));
#39782=CARTESIAN_POINT('Ctrl Pts',(-12.4378151222667,-6.9543694886247,-0.906484242526672));
#39783=CARTESIAN_POINT('Ctrl Pts',(-12.4439512822522,-6.94339503240897,
-0.965698216399908));
#39784=CARTESIAN_POINT('Ctrl Pts',(-12.450680002204,-6.93132701813286,-1.024663045654));
#39785=CARTESIAN_POINT('Ctrl Pts',(-12.4579905368413,-6.91816245718269,
-1.08333333333334));
#39786=CARTESIAN_POINT('',(-13.3303603014234,-7.18268588222787,-1.08333333333334));
#39787=CARTESIAN_POINT('Ctrl Pts',(-12.4579905368413,-6.91816245718265,
-1.08333333333333));
#39788=CARTESIAN_POINT('Ctrl Pts',(-12.6150882655077,-7.02012104908378,
-1.08333333333333));
#39789=CARTESIAN_POINT('Ctrl Pts',(-12.8106174809568,-7.10161229021636,
-1.08333333333333));
#39790=CARTESIAN_POINT('Ctrl Pts',(-13.0925863122299,-7.16596983593587,
-1.08333333333333));
#39791=CARTESIAN_POINT('Ctrl Pts',(-13.2116839714656,-7.18117918553602,
-1.08333333333333));
#39792=CARTESIAN_POINT('Ctrl Pts',(-13.3303603014234,-7.18268588222786,
-1.08333333333333));
#39793=CARTESIAN_POINT('Ctrl Pts',(-13.3303603014234,-7.18268588222788,
-1.08333333333333));
#39794=CARTESIAN_POINT('Ctrl Pts',(-13.312602432605,-7.21564274452362,-0.9568886321034));
#39795=CARTESIAN_POINT('Ctrl Pts',(-13.2978764135175,-7.24268913148589,
-0.828820583351364));
#39796=CARTESIAN_POINT('Ctrl Pts',(-13.2863164700111,-7.26383348564883,
-0.699646919262042));
#39797=CARTESIAN_POINT('Ctrl Pts',(-13.2748173090022,-7.28486666222222,
-0.571152453813466));
#39798=CARTESIAN_POINT('Ctrl Pts',(-13.2664510227833,-7.30005980724142,
-0.441563969171881));
#39799=CARTESIAN_POINT('Ctrl Pts',(-13.2613042752926,-7.30939745578436,
-0.311391073638092));
#39800=CARTESIAN_POINT('Ctrl Pts',(-13.2561988309335,-7.3186601688214,-0.182262827807686));
#39801=CARTESIAN_POINT('Ctrl Pts',(-13.2542614634094,-7.32216103446744,
-0.0525595133522827));
#39802=CARTESIAN_POINT('Ctrl Pts',(-13.2555318677528,-7.31986045983868,
0.0772214321944347));
#39803=CARTESIAN_POINT('Ctrl Pts',(-13.2563983335701,-7.31829137729732,
0.165737150534351));
#39804=CARTESIAN_POINT('Ctrl Pts',(-13.2587560588234,-7.31402308269238,
0.254288981130211));
#39805=CARTESIAN_POINT('Ctrl Pts',(-13.2626054360146,-7.30703628683457,
0.342719102199554));
#39806=CARTESIAN_POINT('Ctrl Pts',(-13.2684086950193,-7.29650310602083,
0.476034927301584));
#39807=CARTESIAN_POINT('Ctrl Pts',(-13.2775701666804,-7.27985434187078,
0.608312350205395));
#39808=CARTESIAN_POINT('Ctrl Pts',(-13.2899434176249,-7.25719547792734,
0.739057191237093));
#39809=CARTESIAN_POINT('Ctrl Pts',(-13.3009290370229,-7.23707775329796,
0.855139299993907));
#39810=CARTESIAN_POINT('Ctrl Pts',(-13.3144456587151,-7.21222189770289,
0.970013302477609));
#39811=CARTESIAN_POINT('Ctrl Pts',(-13.3303603014234,-7.18268588222788,
1.08333333333332));
#39812=CARTESIAN_POINT('',(-15.1266902369927,0.68754979644356,1.08333333333333));
#39813=CARTESIAN_POINT('',(-14.2259398250621,0.827729480997533,1.08333333333333));
#39814=CARTESIAN_POINT('Ctrl Pts',(-15.1266902369927,0.687549796443589,
1.08333333333333));
#39815=CARTESIAN_POINT('Ctrl Pts',(-15.0191128271494,0.737684039417719,
1.08333333333333));
#39816=CARTESIAN_POINT('Ctrl Pts',(-14.905210454464,0.775655426636244,1.08333333333333));
#39817=CARTESIAN_POINT('Ctrl Pts',(-14.6232416231909,0.840012972355744,
1.08333333333333));
#39818=CARTESIAN_POINT('Ctrl Pts',(-14.411718162898,0.851428848194329,1.08333333333333));
#39819=CARTESIAN_POINT('Ctrl Pts',(-14.2259398250622,0.827729480996923,
1.08333333333333));
#39820=CARTESIAN_POINT('',(-15.1266902369927,0.687549796443561,-1.08333333333334));
#39821=CARTESIAN_POINT('Ctrl Pts',(-15.1266902369927,0.687549796443564,
1.08333333333333));
#39822=CARTESIAN_POINT('Ctrl Pts',(-15.1249773086751,0.725235701077295,
0.955915065626697));
#39823=CARTESIAN_POINT('Ctrl Pts',(-15.1234319803901,0.756223536825465,
0.826701571450772));
#39824=CARTESIAN_POINT('Ctrl Pts',(-15.122183667988,0.780412301388329,0.696211209492499));
#39825=CARTESIAN_POINT('Ctrl Pts',(-15.1209550316477,0.804219799510246,
0.567777653525797));
#39826=CARTESIAN_POINT('Ctrl Pts',(-15.12001416535,0.821440959530219,0.438107164856512));
#39827=CARTESIAN_POINT('Ctrl Pts',(-15.1194343523859,0.83197783168462,0.307693975181787));
#39828=CARTESIAN_POINT('Ctrl Pts',(-15.1189800281283,0.840234212474348,
0.205506064179395));
#39829=CARTESIAN_POINT('Ctrl Pts',(-15.1187464308798,0.844386527178334,
0.102862147741089));
#39830=CARTESIAN_POINT('Ctrl Pts',(-15.1187464308798,0.844386527178334,
-1.99840144432528E-15));
#39831=CARTESIAN_POINT('Ctrl Pts',(-15.1187464308798,0.844386527178334,
-0.130666807305563));
#39832=CARTESIAN_POINT('Ctrl Pts',(-15.1191251529677,0.837684329050672,
-0.261069786498716));
#39833=CARTESIAN_POINT('Ctrl Pts',(-15.1198518432089,0.824355801783686,
-0.3907104508711));
#39834=CARTESIAN_POINT('Ctrl Pts',(-15.1205872590302,0.810867235029684,
-0.521907748246278));
#39835=CARTESIAN_POINT('Ctrl Pts',(-15.1216790167187,0.790592205023353,
-0.652324314224286));
#39836=CARTESIAN_POINT('Ctrl Pts',(-15.1230415909943,0.763606761086714,
-0.78144348920301));
#39837=CARTESIAN_POINT('Ctrl Pts',(-15.1241128691977,0.742390363261972,
-0.882959098491598));
#39838=CARTESIAN_POINT('Ctrl Pts',(-15.1253504648421,0.717025942629857,
-0.983672743459549));
#39839=CARTESIAN_POINT('Ctrl Pts',(-15.1266902369927,0.687549796443564,
-1.08333333333333));
#39840=CARTESIAN_POINT('',(-14.2259398250711,0.827729480998061,-1.08333333333334));
#39841=CARTESIAN_POINT('Ctrl Pts',(-15.1266902369927,0.687549796443589,
-1.08333333333333));
#39842=CARTESIAN_POINT('Ctrl Pts',(-15.0191128271494,0.73768403941772,-1.08333333333333));
#39843=CARTESIAN_POINT('Ctrl Pts',(-14.905210454464,0.775655426636245,-1.08333333333333));
#39844=CARTESIAN_POINT('Ctrl Pts',(-14.6232416231937,0.840012972355103,
-1.08333333333333));
#39845=CARTESIAN_POINT('Ctrl Pts',(-14.4117181629048,0.851428848194163,
-1.08333333333333));
#39846=CARTESIAN_POINT('Ctrl Pts',(-14.2259398250711,0.827729480998062,
-1.08333333333333));
#39847=CARTESIAN_POINT('Ctrl Pts',(-14.2259398250621,0.827729480996948,
-1.08333333333319));
#39848=CARTESIAN_POINT('Ctrl Pts',(-14.2239464151202,0.86198962338768,-0.949622058007746));
#39849=CARTESIAN_POINT('Ctrl Pts',(-14.2222079250172,0.889808711690097,
-0.814376693553578));
#39850=CARTESIAN_POINT('Ctrl Pts',(-14.2208398148552,0.911161325029729,
-0.678132403728685));
#39851=CARTESIAN_POINT('Ctrl Pts',(-14.2194782068654,0.932412456504284,
-0.542535637671376));
#39852=CARTESIAN_POINT('Ctrl Pts',(-14.2184834780892,0.947258512328182,
-0.405949418799462));
#39853=CARTESIAN_POINT('Ctrl Pts',(-14.2179179597194,0.955671957675903,
-0.268901316712362));
#39854=CARTESIAN_POINT('Ctrl Pts',(-14.2175487034788,0.961165532005871,
-0.179415511019154));
#39855=CARTESIAN_POINT('Ctrl Pts',(-14.2173613909827,0.963916530719958,
-0.0897327832368514));
#39856=CARTESIAN_POINT('Ctrl Pts',(-14.2173613909827,0.963916530719958,
1.77635683940025E-15));
#39857=CARTESIAN_POINT('Ctrl Pts',(-14.2173613909827,0.963916530719959,
0.137573936980362));
#39858=CARTESIAN_POINT('Ctrl Pts',(-14.2178040883167,0.957451598945575,
0.274951212619699));
#39859=CARTESIAN_POINT('Ctrl Pts',(-14.2186598102071,0.944570379379332,
0.411612406214706));
#39860=CARTESIAN_POINT('Ctrl Pts',(-14.2195221530139,0.931589494866292,
0.549330978772852));
#39861=CARTESIAN_POINT('Ctrl Pts',(-14.2208039138492,0.912092599491199,
0.686322345436968));
#39862=CARTESIAN_POINT('Ctrl Pts',(-14.222421741201,0.886126297665223,0.82205493534731));
#39863=CARTESIAN_POINT('Ctrl Pts',(-14.2234666476786,0.869355437073727,
0.909720570537294));
#39864=CARTESIAN_POINT('Ctrl Pts',(-14.2246506698206,0.849885807806941,
0.996861109122796));
#39865=CARTESIAN_POINT('Ctrl Pts',(-14.2259398250621,0.827729480996951,
1.08333333333318));
#39866=CARTESIAN_POINT('Origin',(-13.892722748591,-3.17092330887753,-3.20017169526126E-15));
#39867=CARTESIAN_POINT('',(-13.6476999686241,-6.55970790622096,-1.08333333333334));
#39868=CARTESIAN_POINT('',(-13.1366786991091,-6.483368720524,-1.08333333333334));
#39869=CARTESIAN_POINT('Origin',(-13.892722748591,-3.17092330887753,-1.08333333333334));
#39870=CARTESIAN_POINT('',(-14.6487667980729,0.141522102768936,-1.08333333333334));
#39871=CARTESIAN_POINT('Origin',(-13.892722748591,-3.17092330887753,-3.20017169526126E-15));
#39872=CARTESIAN_POINT('',(-15.1423033840733,-0.0114224867028857,-1.08333333333334));
#39873=CARTESIAN_POINT('Origin',(-13.892722748591,-3.17092330887753,-1.08333333333334));
#39874=CARTESIAN_POINT('',(-15.1423033840733,-0.0114224867028862,1.08333333333333));
#39875=CARTESIAN_POINT('Ctrl Pts',(-15.1423033840733,-0.0114224867028739,
-1.08333333333334));
#39876=CARTESIAN_POINT('Ctrl Pts',(-15.1423953499066,0.110492695607543,
-0.727666221822802));
#39877=CARTESIAN_POINT('Ctrl Pts',(-15.1413590080604,0.169498193350012,
-0.352782973842781));
#39878=CARTESIAN_POINT('Ctrl Pts',(-15.1413590080604,0.169498193350012,
-2.67362166230902E-15));
#39879=CARTESIAN_POINT('Ctrl Pts',(-15.1413590080604,0.169498193350012,
0.352782973842775));
#39880=CARTESIAN_POINT('Ctrl Pts',(-15.1423953499066,0.110492695607543,
0.727666221822795));
#39881=CARTESIAN_POINT('Ctrl Pts',(-15.1423033840733,-0.0114224867028737,
1.08333333333334));
#39882=CARTESIAN_POINT('',(-14.2484814298548,0.20803111085057,1.08333333333333));
#39883=CARTESIAN_POINT('Origin',(-13.892722748591,-3.17092330887754,1.08333333333333));
#39884=CARTESIAN_POINT('',(-14.2484814298548,0.208031110850571,-1.08333333333334));
#39885=CARTESIAN_POINT('Ctrl Pts',(-14.2484814298548,0.208031110850584,
1.08333333333333));
#39886=CARTESIAN_POINT('Ctrl Pts',(-14.2468058395578,0.322795758952019,
0.725928647976579));
#39887=CARTESIAN_POINT('Ctrl Pts',(-14.2449910310593,0.37779693624925,0.352039859176988));
#39888=CARTESIAN_POINT('Ctrl Pts',(-14.2449910310593,0.37779693624925,-2.46631154156404E-15));
#39889=CARTESIAN_POINT('Ctrl Pts',(-14.2449910310593,0.37779693624925,-0.352039859176994));
#39890=CARTESIAN_POINT('Ctrl Pts',(-14.2468058395578,0.322795758952019,
-0.725928647976587));
#39891=CARTESIAN_POINT('Ctrl Pts',(-14.2484814298548,0.208031110850583,
-1.08333333333334));
#39892=CARTESIAN_POINT('Origin',(-13.892722748591,-3.17092330887753,-1.08333333333334));
#39893=CARTESIAN_POINT('',(-12.7471768669563,-6.36961395396413,-1.08333333333334));
#39894=CARTESIAN_POINT('Origin',(-13.892722748591,-3.17092330887753,-1.08333333333334));
#39895=CARTESIAN_POINT('',(-12.7471768669563,-6.36961395396413,1.08333333333333));
#39896=CARTESIAN_POINT('Ctrl Pts',(-12.7471768669563,-6.36961395396412,
-1.08333333333334));
#39897=CARTESIAN_POINT('Ctrl Pts',(-12.6958726976266,-6.472286317656,-0.725928647976585));
#39898=CARTESIAN_POINT('Ctrl Pts',(-12.6703734952066,-6.52105325020167,
-0.352039859176994));
#39899=CARTESIAN_POINT('Ctrl Pts',(-12.6703734952066,-6.52105325020167,
0.352039859176985));
#39900=CARTESIAN_POINT('Ctrl Pts',(-12.6958726976266,-6.472286317656,0.725928647976577));
#39901=CARTESIAN_POINT('Ctrl Pts',(-12.7471768669563,-6.36961395396412,
1.08333333333333));
#39902=CARTESIAN_POINT('',(-13.6476999686241,-6.55970790622096,1.08333333333333));
#39903=CARTESIAN_POINT('Origin',(-13.892722748591,-3.17092330887754,1.08333333333333));
#39904=CARTESIAN_POINT('Ctrl Pts',(-13.6476999686241,-6.55970790622096,
1.08333333333332));
#39905=CARTESIAN_POINT('Ctrl Pts',(-13.5948858118208,-6.66958959248691,
0.727666221822788));
#39906=CARTESIAN_POINT('Ctrl Pts',(-13.5683505740919,-6.72230205711272,
0.35278297384277));
#39907=CARTESIAN_POINT('Ctrl Pts',(-13.5683505740919,-6.72230205711272,
-0.352782973842779));
#39908=CARTESIAN_POINT('Ctrl Pts',(-13.5948858118208,-6.66958959248691,
-0.727666221822796));
#39909=CARTESIAN_POINT('Ctrl Pts',(-13.6476999686241,-6.55970790622096,
-1.08333333333333));
#39910=CARTESIAN_POINT('',(-13.0227870731057,-2.97236616780882,3.45272288248773));
#39911=CARTESIAN_POINT('Origin',(-13.0227870731057,-2.97236616780882,-2.99978307628674E-15));
#39912=CARTESIAN_POINT('',(-14.7626584240763,-3.36948044994625,3.45272288248773));
#39913=CARTESIAN_POINT('Origin',(-14.7626584240763,-3.36948044994625,-3.40056031423578E-15));
#39914=CARTESIAN_POINT('Origin',(-6.18284328242512,-12.8388063676095,-4.97613300162231E-15));
#39915=CARTESIAN_POINT('',(-6.57000108040694,-13.6427478189686,-3.96060240207311));
#39916=CARTESIAN_POINT('Origin',(-6.57000108040694,-13.6427478189686,-5.28772891427451E-15));
#39917=CARTESIAN_POINT('',(-5.79568548444331,-12.0348649162504,-3.96060240207311));
#39918=CARTESIAN_POINT('Origin',(-6.18284328242512,-12.8388063676095,-2.51985201161581));
#39919=CARTESIAN_POINT('Origin',(-5.79568548444331,-12.0348649162504,-4.66453708897012E-15));
#39920=CARTESIAN_POINT('',(-2.35859284151935,-14.0534529496467,1.08333333333333));
#39921=CARTESIAN_POINT('',(-2.69569375163562,-14.9004267538186,1.08333333333333));
#39922=CARTESIAN_POINT('Ctrl Pts',(-2.35859284151934,-14.0534529496467,
1.08333333333333));
#39923=CARTESIAN_POINT('Ctrl Pts',(-2.37682723618162,-14.2398470420046,
1.08333333333333));
#39924=CARTESIAN_POINT('Ctrl Pts',(-2.43502529011671,-14.4435268961719,
1.08333333333332));
#39925=CARTESIAN_POINT('Ctrl Pts',(-2.56051322547963,-14.7041052789647,
1.08333333333333));
#39926=CARTESIAN_POINT('Ctrl Pts',(-2.62287825309305,-14.806702452812,1.08333333333333));
#39927=CARTESIAN_POINT('Ctrl Pts',(-2.69569375163558,-14.9004267538186,
1.08333333333333));
#39928=CARTESIAN_POINT('',(-2.35859284151935,-14.0534529496467,-1.08333333333334));
#39929=CARTESIAN_POINT('Ctrl Pts',(-2.35859284151935,-14.0534529496467,
1.08333333333333));
#39930=CARTESIAN_POINT('Ctrl Pts',(-2.32474809698527,-14.0591331175362,
0.949622058007895));
#39931=CARTESIAN_POINT('Ctrl Pts',(-2.29723964086638,-14.0636285445206,
0.814376693553736));
#39932=CARTESIAN_POINT('Ctrl Pts',(-2.27611794897253,-14.0670461391994,
0.678132403728853));
#39933=CARTESIAN_POINT('Ctrl Pts',(-2.25509664145098,-14.0704474911881,
0.542535637671543));
#39934=CARTESIAN_POINT('Ctrl Pts',(-2.24040145926613,-14.0727812605466,
0.405949418799629));
#39935=CARTESIAN_POINT('Ctrl Pts',(-2.23207311688321,-14.0741020886196,
0.268901316712528));
#39936=CARTESIAN_POINT('Ctrl Pts',(-2.22663511068775,-14.0749645256946,
0.179415511019263));
#39937=CARTESIAN_POINT('Ctrl Pts',(-2.2239114043034,-14.075394064317,0.0897327832369026));
#39938=CARTESIAN_POINT('Ctrl Pts',(-2.2239114043034,-14.075394064317,-8.43769498715119E-15));
#39939=CARTESIAN_POINT('Ctrl Pts',(-2.2239114043034,-14.075394064317,-0.137573936980349));
#39940=CARTESIAN_POINT('Ctrl Pts',(-2.23031275616482,-14.0743870796481,
-0.274951212619667));
#39941=CARTESIAN_POINT('Ctrl Pts',(-2.24306143269717,-14.0723550057958,
-0.411612406214657));
#39942=CARTESIAN_POINT('Ctrl Pts',(-2.25590874866049,-14.0703072093226,
-0.549330978772813));
#39943=CARTESIAN_POINT('Ctrl Pts',(-2.27520203478074,-14.0672183663696,
-0.68632234543694));
#39944=CARTESIAN_POINT('Ctrl Pts',(-2.30087730766032,-14.0630175856782,
-0.822054935347292));
#39945=CARTESIAN_POINT('Ctrl Pts',(-2.31746020132759,-14.0603044266067,
-0.909720570537337));
#39946=CARTESIAN_POINT('Ctrl Pts',(-2.33670515605249,-14.0571263627534,
-0.996861109122898));
#39947=CARTESIAN_POINT('Ctrl Pts',(-2.35859284151935,-14.0534529496467,
-1.08333333333334));
#39948=CARTESIAN_POINT('',(-2.69569375163563,-14.9004267538187,-1.08333333333334));
#39949=CARTESIAN_POINT('Ctrl Pts',(-2.35859284151934,-14.0534529496467,
-1.08333333333333));
#39950=CARTESIAN_POINT('Ctrl Pts',(-2.37688304383397,-14.2404175142851,
-1.08333333333333));
#39951=CARTESIAN_POINT('Ctrl Pts',(-2.43503901504648,-14.4435553962822,
-1.08333333333334));
#39952=CARTESIAN_POINT('Ctrl Pts',(-2.56054033827446,-14.7041615792632,
-1.08333333333334));
#39953=CARTESIAN_POINT('Ctrl Pts',(-2.62284674626764,-14.8066618988743,
-1.08333333333334));
#39954=CARTESIAN_POINT('Ctrl Pts',(-2.69569375163563,-14.9004267538187,
-1.08333333333334));
#39955=CARTESIAN_POINT('Ctrl Pts',(-2.69569375163559,-14.9004267538186,
-1.08333333333335));
#39956=CARTESIAN_POINT('Ctrl Pts',(-2.65857154890325,-14.9071426748862,
-0.955915065626573));
#39957=CARTESIAN_POINT('Ctrl Pts',(-2.628016775001,-14.9125315333598,-0.826701571450498));
#39958=CARTESIAN_POINT('Ctrl Pts',(-2.60415669762586,-14.9166970252376,
-0.696211209492072));
#39959=CARTESIAN_POINT('Ctrl Pts',(-2.58067270588166,-14.9207968600927,
-0.567777653525379));
#39960=CARTESIAN_POINT('Ctrl Pts',(-2.56367395385075,-14.923711651889,-0.438107164856101));
#39961=CARTESIAN_POINT('Ctrl Pts',(-2.55327224255806,-14.9254910506792,
-0.307693975181385));
#39962=CARTESIAN_POINT('Ctrl Pts',(-2.54512176981446,-14.9268853348437,
-0.205506064179128));
#39963=CARTESIAN_POINT('Ctrl Pts',(-2.54102158203148,-14.9275815713119,
-0.102862147740959));
#39964=CARTESIAN_POINT('Ctrl Pts',(-2.54102158203148,-14.9275815713119,
-4.44089209850063E-15));
#39965=CARTESIAN_POINT('Ctrl Pts',(-2.54102158203148,-14.9275815713119,
0.130666807305524));
#39966=CARTESIAN_POINT('Ctrl Pts',(-2.54764001565181,-14.9264594186595,
0.261069786498646));
#39967=CARTESIAN_POINT('Ctrl Pts',(-2.56079607270382,-14.9242020129234,
0.390710450870999));
#39968=CARTESIAN_POINT('Ctrl Pts',(-2.57411009834303,-14.9219175018628,
0.521907748246163));
#39969=CARTESIAN_POINT('Ctrl Pts',(-2.59411972995703,-14.9184702682937,
0.652324314224157));
#39970=CARTESIAN_POINT('Ctrl Pts',(-2.62073179377387,-14.9137938537994,
0.781443489202868));
#39971=CARTESIAN_POINT('Ctrl Pts',(-2.64165463403551,-14.9101171801624,
0.882959098491507));
#39972=CARTESIAN_POINT('Ctrl Pts',(-2.66665850662476,-14.9056796321318,
0.983672743459509));
#39973=CARTESIAN_POINT('Ctrl Pts',(-2.69569375163559,-14.9004267538186,
1.08333333333334));
#39974=CARTESIAN_POINT('',(-9.96888517526507,-11.3978423664701,1.08333333333333));
#39975=CARTESIAN_POINT('',(-9.516873369993,-10.6062067328295,1.08333333333333));
#39976=CARTESIAN_POINT('Ctrl Pts',(-9.96888517526507,-11.3978423664701,
1.08333333333333));
#39977=CARTESIAN_POINT('Ctrl Pts',(-9.94100828682427,-11.282476771434,1.08333333333333));
#39978=CARTESIAN_POINT('Ctrl Pts',(-9.89967854500783,-11.1697495378475,
1.08333333333333));
#39979=CARTESIAN_POINT('Ctrl Pts',(-9.77419060964491,-10.9091711550547,
1.08333333333333));
#39980=CARTESIAN_POINT('Ctrl Pts',(-9.65123318042897,-10.7366777723525,
1.08333333333333));
#39981=CARTESIAN_POINT('Ctrl Pts',(-9.51687336999256,-10.6062067328299,
1.08333333333333));
#39982=CARTESIAN_POINT('',(-9.96888517526507,-11.3978423664701,-1.08333333333334));
#39983=CARTESIAN_POINT('Ctrl Pts',(-9.96888517526508,-11.3978423664701,
1.08333333333333));
#39984=CARTESIAN_POINT('Ctrl Pts',(-9.99706424266063,-11.3731961327199,
0.956888632103256));
#39985=CARTESIAN_POINT('Ctrl Pts',(-10.020155672713,-11.3528209383891,0.828820583351071));
#39986=CARTESIAN_POINT('Ctrl Pts',(-10.038197564346,-11.3368457653652,0.699646919261599));
#39987=CARTESIAN_POINT('Ctrl Pts',(-10.0561445912219,-11.3209545902358,
0.571152453812953));
#39988=CARTESIAN_POINT('Ctrl Pts',(-10.0690951385517,-11.3094172714603,
0.441563969171296));
#39989=CARTESIAN_POINT('Ctrl Pts',(-10.0770534136919,-11.3023217413999,
0.311391073637437));
#39990=CARTESIAN_POINT('Ctrl Pts',(-10.0849478229272,-11.2952831536342,
0.182262827807044));
#39991=CARTESIAN_POINT('Ctrl Pts',(-10.0879298097314,-11.2926153440655,
0.0525595133516554));
#39992=CARTESIAN_POINT('Ctrl Pts',(-10.0859696068728,-11.2943658227348,
-0.0772214321950453));
#39993=CARTESIAN_POINT('Ctrl Pts',(-10.0846326712896,-11.2955597181575,
-0.165737150534751));
#39994=CARTESIAN_POINT('Ctrl Pts',(-10.0809960349672,-11.2988081152181,
-0.2542889811304));
#39995=CARTESIAN_POINT('Ctrl Pts',(-10.0750409796764,-11.304115688826,-0.342719102199531));
#39996=CARTESIAN_POINT('Ctrl Pts',(-10.0660632343107,-11.3121173012435,
-0.476034927301883));
#39997=CARTESIAN_POINT('Ctrl Pts',(-10.0518705086679,-11.3247537742305,
-0.608312350206005));
#39998=CARTESIAN_POINT('Ctrl Pts',(-10.0325330571073,-11.3418588735079,
-0.739057191238004));
#39999=CARTESIAN_POINT('Ctrl Pts',(-10.0153642561251,-11.3570456753652,
-0.855139299994515));
#40000=CARTESIAN_POINT('Ctrl Pts',(-9.99413932000721,-11.3757543553326,
-0.970013302477919));
#40001=CARTESIAN_POINT('Ctrl Pts',(-9.96888517526508,-11.3978423664701,
-1.08333333333334));
#40002=CARTESIAN_POINT('',(-9.51687336999906,-10.6062067328363,-1.08333333333334));
#40003=CARTESIAN_POINT('Ctrl Pts',(-9.96888517526507,-11.3978423664701,
-1.08333333333333));
#40004=CARTESIAN_POINT('Ctrl Pts',(-9.94100828682427,-11.282476771434,-1.08333333333333));
#40005=CARTESIAN_POINT('Ctrl Pts',(-9.89967854500783,-11.1697495378475,
-1.08333333333333));
#40006=CARTESIAN_POINT('Ctrl Pts',(-9.77419060964618,-10.9091711550573,
-1.08333333333333));
#40007=CARTESIAN_POINT('Ctrl Pts',(-9.6512331804331,-10.7366777723579,-1.08333333333333));
#40008=CARTESIAN_POINT('Ctrl Pts',(-9.51687336999908,-10.6062067328363,
-1.08333333333333));
#40009=CARTESIAN_POINT('Ctrl Pts',(-9.51687336999256,-10.6062067328299,
-1.08333333333319));
#40010=CARTESIAN_POINT('Ctrl Pts',(-9.54248335115827,-10.5832270800755,
-0.949270311030248));
#40011=CARTESIAN_POINT('Ctrl Pts',(-9.56321910180067,-10.5644593135702,
-0.813521288367661));
#40012=CARTESIAN_POINT('Ctrl Pts',(-9.57910097474595,-10.5500390764974,
-0.676607052100613));
#40013=CARTESIAN_POINT('Ctrl Pts',(-9.59267821366648,-10.5377113740467,
-0.559560573777554));
#40014=CARTESIAN_POINT('Ctrl Pts',(-9.6027075928823,-10.5285603838747,-0.44166251627891));
#40015=CARTESIAN_POINT('Ctrl Pts',(-9.6091818848891,-10.5226481221753,-0.323238258334718));
#40016=CARTESIAN_POINT('Ctrl Pts',(-9.61666296645239,-10.5158164698571,
-0.186398348762648));
#40017=CARTESIAN_POINT('Ctrl Pts',(-9.61937600851194,-10.5133302394117,
-0.0492519096262118));
#40018=CARTESIAN_POINT('Ctrl Pts',(-9.61735300288125,-10.5151805128572,
0.08767582706605));
#40019=CARTESIAN_POINT('Ctrl Pts',(-9.61532413250719,-10.5170361502911,
0.225000520654331));
#40020=CARTESIAN_POINT('Ctrl Pts',(-9.60853168799772,-10.5232534570122,
0.362105241912796));
#40021=CARTESIAN_POINT('Ctrl Pts',(-9.59697252030892,-10.5337846211338,
0.498460177595657));
#40022=CARTESIAN_POINT('Ctrl Pts',(-9.5853634847053,-10.5443612182148,0.635403368116659));
#40023=CARTESIAN_POINT('Ctrl Pts',(-9.56894645381043,-10.5592890006364,
0.771590289741169));
#40024=CARTESIAN_POINT('Ctrl Pts',(-9.54768316346852,-10.578480335569,0.906484242526434));
#40025=CARTESIAN_POINT('Ctrl Pts',(-9.53834928383367,-10.5869046954593,
0.965698216399696));
#40026=CARTESIAN_POINT('Ctrl Pts',(-9.52808112091929,-10.5961500981613,
1.02466304565381));
#40027=CARTESIAN_POINT('Ctrl Pts',(-9.51687336999256,-10.6062067328299,
1.08333333333318));
#40028=CARTESIAN_POINT('Origin',(-6.18284328242512,-12.8388063676095,-4.97613300162231E-15));
#40029=CARTESIAN_POINT('',(-3.38061559238688,-14.7601124814492,-1.08333333333334));
#40030=CARTESIAN_POINT('',(-3.12168342103518,-14.3129832609672,-1.08333333333334));
#40031=CARTESIAN_POINT('Origin',(-6.18284328242512,-12.8388063676095,-1.08333333333334));
#40032=CARTESIAN_POINT('',(-9.24400314381506,-11.3646294742518,-1.08333333333334));
#40033=CARTESIAN_POINT('Origin',(-6.18284328242512,-12.8388063676095,-4.97613300162231E-15));
#40034=CARTESIAN_POINT('',(-9.43214127690829,-11.8458513067218,-1.08333333333334));
#40035=CARTESIAN_POINT('Origin',(-6.18284328242512,-12.8388063676095,-1.08333333333334));
#40036=CARTESIAN_POINT('',(-9.43214127690829,-11.8458513067218,1.08333333333333));
#40037=CARTESIAN_POINT('Ctrl Pts',(-9.43214127690829,-11.8458513067218,
-1.08333333333333));
#40038=CARTESIAN_POINT('Ctrl Pts',(-9.52751574438859,-11.7699103356433,
-0.727666221822795));
#40039=CARTESIAN_POINT('Ctrl Pts',(-9.57300195158999,-11.7323107648653,
-0.352782973842778));
#40040=CARTESIAN_POINT('Ctrl Pts',(-9.57300195158999,-11.7323107648653,
-4.85994849902029E-15));
#40041=CARTESIAN_POINT('Ctrl Pts',(-9.57300195158999,-11.7323107648653,
0.352782973842767));
#40042=CARTESIAN_POINT('Ctrl Pts',(-9.52751574438859,-11.7699103356433,
0.727666221822782));
#40043=CARTESIAN_POINT('Ctrl Pts',(-9.43214127690829,-11.8458513067218,
1.08333333333332));
#40044=CARTESIAN_POINT('',(-9.04642813528379,-11.0102060831369,1.08333333333333));
#40045=CARTESIAN_POINT('Origin',(-6.18284328242512,-12.8388063676095,1.08333333333333));
#40046=CARTESIAN_POINT('',(-9.04642813528379,-11.0102060831369,-1.08333333333334));
#40047=CARTESIAN_POINT('Ctrl Pts',(-9.0464281352838,-11.0102060831369,1.08333333333332));
#40048=CARTESIAN_POINT('Ctrl Pts',(-9.13511003678158,-10.9373414661859,
0.725928647976571));
#40049=CARTESIAN_POINT('Ctrl Pts',(-9.17698017417422,-10.901629918632,0.352039859176983));
#40050=CARTESIAN_POINT('Ctrl Pts',(-9.17698017417422,-10.901629918632,-4.5383086406711E-15));
#40051=CARTESIAN_POINT('Ctrl Pts',(-9.17698017417422,-10.901629918632,-0.352039859176993));
#40052=CARTESIAN_POINT('Ctrl Pts',(-9.13511003678158,-10.9373414661859,
-0.725928647976581));
#40053=CARTESIAN_POINT('Ctrl Pts',(-9.0464281352838,-11.0102060831369,-1.08333333333333));
#40054=CARTESIAN_POINT('Origin',(-6.18284328242512,-12.8388063676095,-1.08333333333334));
#40055=CARTESIAN_POINT('',(-2.96777005865995,-13.9375335292483,-1.08333333333334));
#40056=CARTESIAN_POINT('Origin',(-6.18284328242512,-12.8388063676095,-1.08333333333334));
#40057=CARTESIAN_POINT('',(-2.96777005865995,-13.9375335292483,1.08333333333333));
#40058=CARTESIAN_POINT('Ctrl Pts',(-2.96777005865994,-13.9375335292483,
-1.08333333333334));
#40059=CARTESIAN_POINT('Ctrl Pts',(-2.85550994597631,-13.9614374861791,
-0.725928647976589));
#40060=CARTESIAN_POINT('Ctrl Pts',(-2.80148393014434,-13.9719070920595,
-0.352039859176996));
#40061=CARTESIAN_POINT('Ctrl Pts',(-2.80148393014434,-13.9719070920595,
0.352039859176986));
#40062=CARTESIAN_POINT('Ctrl Pts',(-2.85550994597631,-13.9614374861791,
0.725928647976578));
#40063=CARTESIAN_POINT('Ctrl Pts',(-2.96777005865994,-13.9375335292483,
1.08333333333333));
#40064=CARTESIAN_POINT('',(-3.38061559238688,-14.7601124814492,1.08333333333333));
#40065=CARTESIAN_POINT('Origin',(-6.18284328242512,-12.8388063676095,1.08333333333333));
#40066=CARTESIAN_POINT('Ctrl Pts',(-3.38061559238688,-14.7601124814492,
1.08333333333333));
#40067=CARTESIAN_POINT('Ctrl Pts',(-3.26177754255684,-14.7873308217382,
0.727666221822789));
#40068=CARTESIAN_POINT('Ctrl Pts',(-3.20402082808,-14.799450421612,0.35278297384277));
#40069=CARTESIAN_POINT('Ctrl Pts',(-3.20402082808,-14.799450421612,-0.352782973842781));
#40070=CARTESIAN_POINT('Ctrl Pts',(-3.26177754255684,-14.7873308217382,
-0.727666221822799));
#40071=CARTESIAN_POINT('Ctrl Pts',(-3.38061559238688,-14.7601124814492,
-1.08333333333334));
#40072=CARTESIAN_POINT('',(-5.79568548444331,-12.0348649162504,3.45272288248773));
#40073=CARTESIAN_POINT('Origin',(-5.79568548444331,-12.0348649162504,-4.66453708897012E-15));
#40074=CARTESIAN_POINT('',(-6.57000108040694,-13.6427478189686,3.45272288248772));
#40075=CARTESIAN_POINT('Origin',(-6.57000108040694,-13.6427478189686,-5.28772891427451E-15));
#40076=CARTESIAN_POINT('Origin',(6.1828432824253,-12.8388063676094,-4.9761330016223E-15));
#40077=CARTESIAN_POINT('',(6.57000108040713,-13.6427478189685,-3.96060240207311));
#40078=CARTESIAN_POINT('Origin',(6.57000108040713,-13.6427478189685,-5.28772891427449E-15));
#40079=CARTESIAN_POINT('',(5.79568548444348,-12.0348649162503,-3.96060240207311));
#40080=CARTESIAN_POINT('Origin',(6.1828432824253,-12.8388063676094,-2.51985201161581));
#40081=CARTESIAN_POINT('Origin',(5.79568548444348,-12.0348649162504,-4.66453708897011E-15));
#40082=CARTESIAN_POINT('',(9.51687336999268,-10.6062067328298,1.08333333333333));
#40083=CARTESIAN_POINT('',(9.96888517526453,-11.3978423664706,1.08333333333333));
#40084=CARTESIAN_POINT('Ctrl Pts',(9.5168733699927,-10.6062067328298,1.08333333333333));
#40085=CARTESIAN_POINT('Ctrl Pts',(9.65164439811578,-10.737077088181,1.08333333333333));
#40086=CARTESIAN_POINT('Ctrl Pts',(9.77420433457484,-10.9091996551649,1.08333333333333));
#40087=CARTESIAN_POINT('Ctrl Pts',(9.89970565780286,-11.169805838146,1.08333333333333));
#40088=CARTESIAN_POINT('Ctrl Pts',(9.94099622466366,-11.2824268534395,1.08333333333333));
#40089=CARTESIAN_POINT('Ctrl Pts',(9.96888517526534,-11.3978423664704,1.08333333333333));
#40090=CARTESIAN_POINT('',(9.51687336999268,-10.6062067328298,-1.08333333333334));
#40091=CARTESIAN_POINT('Ctrl Pts',(9.51687336999268,-10.6062067328298,1.08333333333333));
#40092=CARTESIAN_POINT('Ctrl Pts',(9.54241615713793,-10.5832873727889,0.949622058007762));
#40093=CARTESIAN_POINT('Ctrl Pts',(9.56308206533645,-10.5645832486408,0.814376693553466));
#40094=CARTESIAN_POINT('Ctrl Pts',(9.5789232079445,-10.5502004803844,0.678132403728444));
#40095=CARTESIAN_POINT('Ctrl Pts',(9.59468906287363,-10.5358860686389,0.542535637671145));
#40096=CARTESIAN_POINT('Ctrl Pts',(9.60567597345963,-10.5258519939611,0.405949418799242));
#40097=CARTESIAN_POINT('Ctrl Pts',(9.61190127497217,-10.5201641565229,0.268901316712153));
#40098=CARTESIAN_POINT('Ctrl Pts',(9.61596609683434,-10.5164502727984,0.179415511019018));
#40099=CARTESIAN_POINT('Ctrl Pts',(9.61800012680612,-10.5145886063487,0.0897327832367887));
#40100=CARTESIAN_POINT('Ctrl Pts',(9.61800012680612,-10.5145886063487,9.32587340685131E-15));
#40101=CARTESIAN_POINT('Ctrl Pts',(9.61800012680612,-10.5145886063487,-0.137573936980381));
#40102=CARTESIAN_POINT('Ctrl Pts',(9.61322165688595,-10.5189655400926,-0.274951212619743));
#40103=CARTESIAN_POINT('Ctrl Pts',(9.6036842477684,-10.5276658794419,-0.411612406214774));
#40104=CARTESIAN_POINT('Ctrl Pts',(9.59407304553156,-10.5364335353099,-0.54933097877281));
#40105=CARTESIAN_POINT('Ctrl Pts',(9.57962892372621,-10.5495917717182,-0.686322345436814));
#40106=CARTESIAN_POINT('Ctrl Pts',(9.5603363503304,-10.5670463644555,-0.822054935347047));
#40107=CARTESIAN_POINT('Ctrl Pts',(9.54787585206456,-10.5783197657831,-0.909720570537174));
#40108=CARTESIAN_POINT('Ctrl Pts',(9.5333921086825,-10.5913845868635,-0.996861109122817));
#40109=CARTESIAN_POINT('Ctrl Pts',(9.51687336999268,-10.6062067328298,-1.08333333333334));
#40110=CARTESIAN_POINT('',(9.9688851752657,-11.3978423664719,-1.08333333333334));
#40111=CARTESIAN_POINT('Ctrl Pts',(9.5168733699927,-10.6062067328298,-1.08333333333333));
#40112=CARTESIAN_POINT('Ctrl Pts',(9.65123318042911,-10.7366777723523,-1.08333333333333));
#40113=CARTESIAN_POINT('Ctrl Pts',(9.77419060964506,-10.9091711550545,-1.08333333333333));
#40114=CARTESIAN_POINT('Ctrl Pts',(9.89967854500826,-11.1697495378479,-1.08333333333333));
#40115=CARTESIAN_POINT('Ctrl Pts',(9.94100828682489,-11.2824767714351,-1.08333333333333));
#40116=CARTESIAN_POINT('Ctrl Pts',(9.96888517526571,-11.3978423664719,-1.08333333333333));
#40117=CARTESIAN_POINT('Ctrl Pts',(9.96888517526519,-11.39784236647,-1.08333333333359));
#40118=CARTESIAN_POINT('Ctrl Pts',(9.99728120861575,-11.3730063679711,-0.955915065626921));
#40119=CARTESIAN_POINT('Ctrl Pts',(10.0205449777511,-11.3524775820965,-0.826701571450959));
#40120=CARTESIAN_POINT('Ctrl Pts',(10.038678205356,-11.3364201641361,-0.696211209492648));
#40121=CARTESIAN_POINT('Ctrl Pts',(10.0565256146782,-11.3206158452779,-0.567777653525928));
#40122=CARTESIAN_POINT('Ctrl Pts',(10.0694030392049,-11.309143028737,-0.438107164856624));
#40123=CARTESIAN_POINT('Ctrl Pts',(10.0772795901119,-11.3021200803759,-0.307693975181881));
#40124=CARTESIAN_POINT('Ctrl Pts',(10.0834514220032,-11.2966171061454,-0.20550606417946));
#40125=CARTESIAN_POINT('Ctrl Pts',(10.0865521868617,-11.2938455465903,-0.102862147741125));
#40126=CARTESIAN_POINT('Ctrl Pts',(10.0865521868617,-11.2938455465903,-4.44089209850063E-15));
#40127=CARTESIAN_POINT('Ctrl Pts',(10.0865521868617,-11.2938455465903,0.130666807305562));
#40128=CARTESIAN_POINT('Ctrl Pts',(10.0815483267233,-11.2983203956244,0.261069786498721));
#40129=CARTESIAN_POINT('Ctrl Pts',(10.0715807484455,-11.3071987457576,0.390710450871112));
#40130=CARTESIAN_POINT('Ctrl Pts',(10.0614934865685,-11.3161837008123,0.521907748246463));
#40131=CARTESIAN_POINT('Ctrl Pts',(10.0463225295865,-11.3296785457857,0.652324314224642));
#40132=CARTESIAN_POINT('Ctrl Pts',(10.0260740111135,-11.3475689983448,0.781443489203535));
#40133=CARTESIAN_POINT('Ctrl Pts',(10.0101542943843,-11.3616347650465,0.88295909849203));
#40134=CARTESIAN_POINT('Ctrl Pts',(9.99109522006272,-11.3784168138781,0.983672743459888));
#40135=CARTESIAN_POINT('Ctrl Pts',(9.96888517526519,-11.39784236647,1.08333333333358));
#40136=CARTESIAN_POINT('',(2.69569375163578,-14.9004267538186,1.08333333333333));
#40137=CARTESIAN_POINT('',(2.35859284151893,-14.0534529496468,1.08333333333333));
#40138=CARTESIAN_POINT('Ctrl Pts',(2.6956937516358,-14.9004267538186,1.08333333333332));
#40139=CARTESIAN_POINT('Ctrl Pts',(2.62284674626782,-14.8066618988742,1.08333333333332));
#40140=CARTESIAN_POINT('Ctrl Pts',(2.56054033827465,-14.7041615792632,1.08333333333332));
#40141=CARTESIAN_POINT('Ctrl Pts',(2.4350390150467,-14.4435553962822,1.08333333333332));
#40142=CARTESIAN_POINT('Ctrl Pts',(2.37688304383419,-14.2404175142851,1.08333333333332));
#40143=CARTESIAN_POINT('Ctrl Pts',(2.35859284151955,-14.0534529496467,1.08333333333332));
#40144=CARTESIAN_POINT('',(2.69569375163578,-14.9004267538186,-1.08333333333334));
#40145=CARTESIAN_POINT('Ctrl Pts',(2.69569375163578,-14.9004267538186,1.08333333333333));
#40146=CARTESIAN_POINT('Ctrl Pts',(2.65885518901859,-14.9070913604575,0.956888632103347));
#40147=CARTESIAN_POINT('Ctrl Pts',(2.62852794948137,-14.9124412415715,0.828820583351256));
#40148=CARTESIAN_POINT('Ctrl Pts',(2.60478912083403,-14.9165866029902,0.699646919261879));
#40149=CARTESIAN_POINT('Ctrl Pts',(2.58117511159368,-14.9207101679857,0.571152453813268));
#40150=CARTESIAN_POINT('Ctrl Pts',(2.56408033836306,-14.9236419130061,0.441563969171648));
#40151=CARTESIAN_POINT('Ctrl Pts',(2.55357092618676,-14.9254399524253,0.311391073637824));
#40152=CARTESIAN_POINT('Ctrl Pts',(2.54314585302948,-14.9272235624095,0.182262827807427));
#40153=CARTESIAN_POINT('Ctrl Pts',(2.53920083715778,-14.927891621514,0.0525595133520343));
#40154=CARTESIAN_POINT('Ctrl Pts',(2.54179158298272,-14.9274504788058,-0.077221432194672));
#40155=CARTESIAN_POINT('Ctrl Pts',(2.54355857371286,-14.9271496020974,-0.165737150534507));
#40156=CARTESIAN_POINT('Ctrl Pts',(2.54836567846244,-14.9263317077699,-0.254288981130285));
#40157=CARTESIAN_POINT('Ctrl Pts',(2.55622822284789,-14.9249850760809,-0.342719102199546));
#40158=CARTESIAN_POINT('Ctrl Pts',(2.56808166802554,-14.9229549158531,-0.47603492730158));
#40159=CARTESIAN_POINT('Ctrl Pts',(2.58681028013297,-14.9197373081624,-0.608312350205393));
#40160=CARTESIAN_POINT('Ctrl Pts',(2.61224028910069,-14.9152835347009,-0.739057191237091));
#40161=CARTESIAN_POINT('Ctrl Pts',(2.63481838123332,-14.9113292416576,-0.855139299993913));
#40162=CARTESIAN_POINT('Ctrl Pts',(2.66267894744191,-14.9063995895532,-0.970013302477622));
#40163=CARTESIAN_POINT('Ctrl Pts',(2.69569375163578,-14.9004267538186,-1.08333333333334));
#40164=CARTESIAN_POINT('',(2.35859284152043,-14.0534529496557,-1.08333333333334));
#40165=CARTESIAN_POINT('Ctrl Pts',(2.6956937516358,-14.9004267538186,-1.08333333333334));
#40166=CARTESIAN_POINT('Ctrl Pts',(2.62284674626782,-14.8066618988742,-1.08333333333334));
#40167=CARTESIAN_POINT('Ctrl Pts',(2.56054033827465,-14.7041615792632,-1.08333333333334));
#40168=CARTESIAN_POINT('Ctrl Pts',(2.43503901504795,-14.4435553962848,-1.08333333333334));
#40169=CARTESIAN_POINT('Ctrl Pts',(2.37688304383586,-14.2404175142916,-1.08333333333334));
#40170=CARTESIAN_POINT('Ctrl Pts',(2.35859284152042,-14.0534529496557,-1.08333333333334));
#40171=CARTESIAN_POINT('Ctrl Pts',(2.35859284151951,-14.0534529496467,-1.08333333333319));
#40172=CARTESIAN_POINT('Ctrl Pts',(2.32465906345733,-14.0591480600448,-0.949270311030372));
#40173=CARTESIAN_POINT('Ctrl Pts',(2.29705730368849,-14.0636584116899,-0.813521288367913));
#40174=CARTESIAN_POINT('Ctrl Pts',(2.27588092254449,-14.0670844892038,-0.676607052100994));
#40175=CARTESIAN_POINT('Ctrl Pts',(2.25777746665768,-14.0700134052785,-0.55956057377781));
#40176=CARTESIAN_POINT('Ctrl Pts',(2.24436971878542,-14.0721491406499,-0.441662516279038));
#40177=CARTESIAN_POINT('Ctrl Pts',(2.23571067141573,-14.073524711092,-0.323238258334718));
#40178=CARTESIAN_POINT('Ctrl Pts',(2.2257050924945,-14.0751141906309,-0.186398348762649));
#40179=CARTESIAN_POINT('Ctrl Pts',(2.22206972520347,-14.0756851929985,-0.0492519096262131));
#40180=CARTESIAN_POINT('Ctrl Pts',(2.22477765061414,-14.0752571701311,0.087675827066048));
#40181=CARTESIAN_POINT('Ctrl Pts',(2.22749342636756,-14.0748279064149,0.225000520654297));
#40182=CARTESIAN_POINT('Ctrl Pts',(2.23658933237962,-14.0733937867901,0.362105241912729));
#40183=CARTESIAN_POINT('Ctrl Pts',(2.25202995120888,-14.0709225390114,0.498460177595558));
#40184=CARTESIAN_POINT('Ctrl Pts',(2.26753718309241,-14.0684406299137,0.635403368116538));
#40185=CARTESIAN_POINT('Ctrl Pts',(2.28944404469282,-14.0649125984157,0.771590289741026));
#40186=CARTESIAN_POINT('Ctrl Pts',(2.31770587921582,-14.0602538902201,0.906484242526269));
#40187=CARTESIAN_POINT('Ctrl Pts',(2.33011188776182,-14.0582088717468,0.965698216399587));
#40188=CARTESIAN_POINT('Ctrl Pts',(2.34374232952329,-14.0559453130119,1.02466304565376));
#40189=CARTESIAN_POINT('Ctrl Pts',(2.35859284151951,-14.0534529496467,1.08333333333318));
#40190=CARTESIAN_POINT('Origin',(6.1828432824253,-12.8388063676094,-4.9761330016223E-15));
#40191=CARTESIAN_POINT('',(9.43214127690845,-11.8458513067217,-1.08333333333334));
#40192=CARTESIAN_POINT('',(9.24400314381522,-11.3646294742516,-1.08333333333334));
#40193=CARTESIAN_POINT('Origin',(6.1828432824253,-12.8388063676094,-1.08333333333334));
#40194=CARTESIAN_POINT('',(3.12168342103538,-14.3129832609672,-1.08333333333334));
#40195=CARTESIAN_POINT('Origin',(6.1828432824253,-12.8388063676094,-4.9761330016223E-15));
#40196=CARTESIAN_POINT('',(3.38061559238708,-14.7601124814491,-1.08333333333334));
#40197=CARTESIAN_POINT('Origin',(6.1828432824253,-12.8388063676094,-1.08333333333334));
#40198=CARTESIAN_POINT('',(3.38061559238708,-14.7601124814491,1.08333333333333));
#40199=CARTESIAN_POINT('Ctrl Pts',(3.3806155923871,-14.7601124814491,-1.08333333333334));
#40200=CARTESIAN_POINT('Ctrl Pts',(3.26177754255705,-14.7873308217381,-0.7276662218228));
#40201=CARTESIAN_POINT('Ctrl Pts',(3.20402082808022,-14.7994504216119,-0.35278297384278));
#40202=CARTESIAN_POINT('Ctrl Pts',(3.20402082808022,-14.7994504216119,-5.42337291349619E-15));
#40203=CARTESIAN_POINT('Ctrl Pts',(3.20402082808022,-14.7994504216119,0.352782973842771));
#40204=CARTESIAN_POINT('Ctrl Pts',(3.26177754255705,-14.7873308217381,0.727666221822789));
#40205=CARTESIAN_POINT('Ctrl Pts',(3.3806155923871,-14.7601124814491,1.08333333333333));
#40206=CARTESIAN_POINT('',(2.96777005866014,-13.9375335292483,1.08333333333333));
#40207=CARTESIAN_POINT('Origin',(6.1828432824253,-12.8388063676094,1.08333333333333));
#40208=CARTESIAN_POINT('',(2.96777005866014,-13.9375335292483,-1.08333333333334));
#40209=CARTESIAN_POINT('Ctrl Pts',(2.96777005866014,-13.9375335292483,1.08333333333333));
#40210=CARTESIAN_POINT('Ctrl Pts',(2.85550994597651,-13.9614374861791,0.725928647976575));
#40211=CARTESIAN_POINT('Ctrl Pts',(2.80148393014454,-13.9719070920595,0.352039859176984));
#40212=CARTESIAN_POINT('Ctrl Pts',(2.80148393014454,-13.9719070920595,-5.10230940761107E-15));
#40213=CARTESIAN_POINT('Ctrl Pts',(2.80148393014454,-13.9719070920595,-0.352039859176994));
#40214=CARTESIAN_POINT('Ctrl Pts',(2.85550994597651,-13.9614374861791,-0.725928647976584));
#40215=CARTESIAN_POINT('Ctrl Pts',(2.96777005866014,-13.9375335292483,-1.08333333333334));
#40216=CARTESIAN_POINT('Origin',(6.1828432824253,-12.8388063676094,-1.08333333333334));
#40217=CARTESIAN_POINT('',(9.04642813528394,-11.0102060831368,-1.08333333333334));
#40218=CARTESIAN_POINT('Origin',(6.1828432824253,-12.8388063676094,-1.08333333333334));
#40219=CARTESIAN_POINT('',(9.04642813528394,-11.0102060831368,1.08333333333333));
#40220=CARTESIAN_POINT('Ctrl Pts',(9.04642813528395,-11.0102060831368,-1.08333333333334));
#40221=CARTESIAN_POINT('Ctrl Pts',(9.13511003678174,-10.9373414661857,-0.725928647976586));
#40222=CARTESIAN_POINT('Ctrl Pts',(9.17698017417438,-10.9016299186319,-0.352039859176995));
#40223=CARTESIAN_POINT('Ctrl Pts',(9.17698017417438,-10.9016299186319,0.352039859176985));
#40224=CARTESIAN_POINT('Ctrl Pts',(9.13511003678174,-10.9373414661857,0.725928647976577));
#40225=CARTESIAN_POINT('Ctrl Pts',(9.04642813528396,-11.0102060831368,1.08333333333333));
#40226=CARTESIAN_POINT('',(9.43214127690845,-11.8458513067217,1.08333333333333));
#40227=CARTESIAN_POINT('Origin',(6.1828432824253,-12.8388063676094,1.08333333333333));
#40228=CARTESIAN_POINT('Ctrl Pts',(9.43214127690846,-11.8458513067217,1.08333333333333));
#40229=CARTESIAN_POINT('Ctrl Pts',(9.52751574438876,-11.7699103356432,0.727666221822791));
#40230=CARTESIAN_POINT('Ctrl Pts',(9.57300195159016,-11.7323107648652,0.352782973842771));
#40231=CARTESIAN_POINT('Ctrl Pts',(9.57300195159016,-11.7323107648652,-0.352782973842781));
#40232=CARTESIAN_POINT('Ctrl Pts',(9.52751574438875,-11.7699103356432,-0.7276662218228));
#40233=CARTESIAN_POINT('Ctrl Pts',(9.43214127690846,-11.8458513067217,-1.08333333333334));
#40234=CARTESIAN_POINT('',(5.79568548444348,-12.0348649162504,3.45272288248773));
#40235=CARTESIAN_POINT('Origin',(5.79568548444348,-12.0348649162504,-4.66453708897011E-15));
#40236=CARTESIAN_POINT('',(6.57000108040713,-13.6427478189685,3.45272288248772));
#40237=CARTESIAN_POINT('Origin',(6.57000108040713,-13.6427478189685,-5.28772891427449E-15));
#40238=CARTESIAN_POINT('Origin',(13.892722748591,-3.17092330887735,-3.20017169526122E-15));
#40239=CARTESIAN_POINT('',(14.7626584240763,-3.36948044994605,-3.96060240207311));
#40240=CARTESIAN_POINT('Origin',(14.7626584240763,-3.36948044994605,-3.40056031423575E-15));
#40241=CARTESIAN_POINT('',(13.0227870731057,-2.97236616780864,-3.96060240207311));
#40242=CARTESIAN_POINT('Origin',(13.892722748591,-3.17092330887735,-2.5198520116158));
#40243=CARTESIAN_POINT('Origin',(13.0227870731057,-2.97236616780865,-2.9997830762867E-15));
#40244=CARTESIAN_POINT('',(14.2259398250621,0.827729480997053,1.08333333333333));
#40245=CARTESIAN_POINT('',(15.1266902369927,0.68754979644376,1.08333333333333));
#40246=CARTESIAN_POINT('Ctrl Pts',(14.2259398250621,0.827729480997104,1.08333333333333));
#40247=CARTESIAN_POINT('Ctrl Pts',(14.4122867506183,0.85150138178118,1.08333333333333));
#40248=CARTESIAN_POINT('Ctrl Pts',(14.6232724628281,0.840005933409976,1.08333333333333));
#40249=CARTESIAN_POINT('Ctrl Pts',(14.9052713763609,0.775641521611009,1.08333333333333));
#40250=CARTESIAN_POINT('Ctrl Pts',(15.0190662790554,0.737705732201359,1.08333333333333));
#40251=CARTESIAN_POINT('Ctrl Pts',(15.1266902369927,0.687549796443767,1.08333333333333));
#40252=CARTESIAN_POINT('',(14.2259398250621,0.827729480997055,-1.08333333333334));
#40253=CARTESIAN_POINT('Ctrl Pts',(14.2259398250621,0.8277294809971,1.08333333333334));
#40254=CARTESIAN_POINT('Ctrl Pts',(14.2239464151202,0.861989623387911,0.949622058007612));
#40255=CARTESIAN_POINT('Ctrl Pts',(14.2222079250172,0.889808711690379,0.814376693553152));
#40256=CARTESIAN_POINT('Ctrl Pts',(14.2208398148552,0.911161325030034,0.678132403727965));
#40257=CARTESIAN_POINT('Ctrl Pts',(14.2194782068654,0.932412456504566,0.542535637670654));
#40258=CARTESIAN_POINT('Ctrl Pts',(14.2184834780892,0.947258512328438,0.40594941879874));
#40259=CARTESIAN_POINT('Ctrl Pts',(14.2179179597194,0.955671957676133,0.268901316711642));
#40260=CARTESIAN_POINT('Ctrl Pts',(14.2175487034788,0.961165532006069,0.179415511018676));
#40261=CARTESIAN_POINT('Ctrl Pts',(14.2173613909827,0.963916530720146,0.0897327832366183));
#40262=CARTESIAN_POINT('Ctrl Pts',(14.2173613909827,0.963916530720146,1.06581410364015E-14));
#40263=CARTESIAN_POINT('Ctrl Pts',(14.2173613909827,0.963916530720146,-0.13757393698032));
#40264=CARTESIAN_POINT('Ctrl Pts',(14.2178040883167,0.957451598945758,-0.274951212619625));
#40265=CARTESIAN_POINT('Ctrl Pts',(14.2186598102071,0.944570379379524,-0.411612406214599));
#40266=CARTESIAN_POINT('Ctrl Pts',(14.2195221530139,0.931589494866494,-0.549330978772693));
#40267=CARTESIAN_POINT('Ctrl Pts',(14.2208039138492,0.912092599491427,-0.686322345436757));
#40268=CARTESIAN_POINT('Ctrl Pts',(14.222421741201,0.886126297665472,-0.822054935347047));
#40269=CARTESIAN_POINT('Ctrl Pts',(14.2234666476786,0.869355437073955,-0.909720570537178));
#40270=CARTESIAN_POINT('Ctrl Pts',(14.2246506698206,0.849885807807131,-0.996861109122824));
#40271=CARTESIAN_POINT('Ctrl Pts',(14.2259398250621,0.827729480997101,-1.08333333333335));
#40272=CARTESIAN_POINT('',(15.1266902369927,0.687549796443762,-1.08333333333334));
#40273=CARTESIAN_POINT('Ctrl Pts',(14.2259398250621,0.827729480997104,-1.08333333333333));
#40274=CARTESIAN_POINT('Ctrl Pts',(14.4122867506183,0.85150138178118,-1.08333333333333));
#40275=CARTESIAN_POINT('Ctrl Pts',(14.6232724628281,0.840005933409977,-1.08333333333333));
#40276=CARTESIAN_POINT('Ctrl Pts',(14.9052713763609,0.775641521611009,-1.08333333333333));
#40277=CARTESIAN_POINT('Ctrl Pts',(15.0190662790554,0.73770573220136,-1.08333333333333));
#40278=CARTESIAN_POINT('Ctrl Pts',(15.1266902369927,0.687549796443768,-1.08333333333333));
#40279=CARTESIAN_POINT('Ctrl Pts',(15.1266902369927,0.687549796443768,-1.08333333333334));
#40280=CARTESIAN_POINT('Ctrl Pts',(15.1249773086751,0.725235701077452,-0.955915065626868));
#40281=CARTESIAN_POINT('Ctrl Pts',(15.1234319803901,0.756223536825589,-0.826701571451108));
#40282=CARTESIAN_POINT('Ctrl Pts',(15.122183667988,0.780412301388443,-0.696211209493001));
#40283=CARTESIAN_POINT('Ctrl Pts',(15.1209550316477,0.804219799510377,-0.567777653526322));
#40284=CARTESIAN_POINT('Ctrl Pts',(15.12001416535,0.821440959530357,-0.43810716485706));
#40285=CARTESIAN_POINT('Ctrl Pts',(15.1194343523859,0.831977831684773,-0.307693975182356));
#40286=CARTESIAN_POINT('Ctrl Pts',(15.1189800281283,0.840234212474528,-0.205506064179778));
#40287=CARTESIAN_POINT('Ctrl Pts',(15.1187464308798,0.844386527178536,-0.102862147741283));
#40288=CARTESIAN_POINT('Ctrl Pts',(15.1187464308798,0.844386527178536,-1.99840144432528E-15));
#40289=CARTESIAN_POINT('Ctrl Pts',(15.1187464308798,0.844386527178536,0.130666807305585));
#40290=CARTESIAN_POINT('Ctrl Pts',(15.1191251529677,0.837684329050871,0.261069786498764));
#40291=CARTESIAN_POINT('Ctrl Pts',(15.1198518432089,0.824355801783881,0.390710450871172));
#40292=CARTESIAN_POINT('Ctrl Pts',(15.1205872590302,0.810867235029882,0.521907748246314));
#40293=CARTESIAN_POINT('Ctrl Pts',(15.1216790167187,0.790592205023559,0.652324314224285));
#40294=CARTESIAN_POINT('Ctrl Pts',(15.1230415909943,0.763606761086929,0.781443489202972));
#40295=CARTESIAN_POINT('Ctrl Pts',(15.1241128691977,0.742390363262186,0.882959098491574));
#40296=CARTESIAN_POINT('Ctrl Pts',(15.1253504648421,0.717025942630064,0.983672743459537));
#40297=CARTESIAN_POINT('Ctrl Pts',(15.1266902369927,0.687549796443768,1.08333333333333));
#40298=CARTESIAN_POINT('',(13.3303603014235,-7.18268588222768,1.08333333333333));
#40299=CARTESIAN_POINT('',(12.4579905368411,-6.91816245718305,1.08333333333333));
#40300=CARTESIAN_POINT('Ctrl Pts',(13.3303603014235,-7.18268588222769,1.08333333333333));
#40301=CARTESIAN_POINT('Ctrl Pts',(13.2116326209361,-7.18117853359731,1.08333333333333));
#40302=CARTESIAN_POINT('Ctrl Pts',(13.0926472341269,-7.16598374096113,1.08333333333333));
#40303=CARTESIAN_POINT('Ctrl Pts',(12.8106483205942,-7.10161932916216,1.08333333333333));
#40304=CARTESIAN_POINT('Ctrl Pts',(12.6155690741987,-7.02043310055321,1.08333333333333));
#40305=CARTESIAN_POINT('Ctrl Pts',(12.4579905368414,-6.91816245718254,1.08333333333333));
#40306=CARTESIAN_POINT('',(13.3303603014235,-7.18268588222768,-1.08333333333334));
#40307=CARTESIAN_POINT('Ctrl Pts',(13.3303603014235,-7.18268588222769,1.08333333333333));
#40308=CARTESIAN_POINT('Ctrl Pts',(13.3126024326051,-7.21564274452345,0.956888632103319));
#40309=CARTESIAN_POINT('Ctrl Pts',(13.2978764135175,-7.24268913148574,0.828820583351199));
#40310=CARTESIAN_POINT('Ctrl Pts',(13.2863164700112,-7.26383348564869,0.699646919261793));
#40311=CARTESIAN_POINT('Ctrl Pts',(13.2748173090023,-7.28486666222208,0.57115245381317));
#40312=CARTESIAN_POINT('Ctrl Pts',(13.2664510227834,-7.30005980724128,0.441563969171537));
#40313=CARTESIAN_POINT('Ctrl Pts',(13.2613042752927,-7.30939745578421,0.311391073637702));
#40314=CARTESIAN_POINT('Ctrl Pts',(13.2561988309336,-7.31866016882124,0.182262827807302));
#40315=CARTESIAN_POINT('Ctrl Pts',(13.2542614634095,-7.32216103446727,0.0525595133519065));
#40316=CARTESIAN_POINT('Ctrl Pts',(13.2555318677529,-7.3198604598385,-0.0772214321948015));
#40317=CARTESIAN_POINT('Ctrl Pts',(13.2563983335702,-7.31829137729713,-0.16573715053459));
#40318=CARTESIAN_POINT('Ctrl Pts',(13.2587560588235,-7.31402308269219,-0.254288981130321));
#40319=CARTESIAN_POINT('Ctrl Pts',(13.2626054360147,-7.30703628683439,-0.342719102199534));
#40320=CARTESIAN_POINT('Ctrl Pts',(13.2684086950193,-7.29650310602066,-0.476034927301568));
#40321=CARTESIAN_POINT('Ctrl Pts',(13.2775701666805,-7.2798543418706,-0.608312350205377));
#40322=CARTESIAN_POINT('Ctrl Pts',(13.289943417625,-7.25719547792716,-0.739057191237071));
#40323=CARTESIAN_POINT('Ctrl Pts',(13.300929037023,-7.23707775329776,-0.8551392999939));
#40324=CARTESIAN_POINT('Ctrl Pts',(13.3144456587152,-7.21222189770271,-0.970013302477615));
#40325=CARTESIAN_POINT('Ctrl Pts',(13.3303603014235,-7.18268588222769,-1.08333333333334));
#40326=CARTESIAN_POINT('',(12.4579905368491,-6.91816245718746,-1.08333333333334));
#40327=CARTESIAN_POINT('Ctrl Pts',(13.3303603014235,-7.18268588222769,-1.08333333333333));
#40328=CARTESIAN_POINT('Ctrl Pts',(13.2116326209361,-7.18117853359731,-1.08333333333333));
#40329=CARTESIAN_POINT('Ctrl Pts',(13.0926472341269,-7.16598374096113,-1.08333333333333));
#40330=CARTESIAN_POINT('Ctrl Pts',(12.810648320597,-7.10161932916281,-1.08333333333333));
#40331=CARTESIAN_POINT('Ctrl Pts',(12.6155690742049,-7.020433100556,-1.08333333333333));
#40332=CARTESIAN_POINT('Ctrl Pts',(12.4579905368491,-6.91816245718749,-1.08333333333333));
#40333=CARTESIAN_POINT('Ctrl Pts',(12.4579905368414,-6.91816245718254,-1.08333333333318));
#40334=CARTESIAN_POINT('Ctrl Pts',(12.4412857888865,-6.94824379644432,-0.949270311030419));
#40335=CARTESIAN_POINT('Ctrl Pts',(12.4276027080704,-6.97263587945666,-0.813521288368017));
#40336=CARTESIAN_POINT('Ctrl Pts',(12.4170780656486,-6.99132836531005,-0.676607052101155));
#40337=CARTESIAN_POINT('Ctrl Pts',(12.4080806643215,-7.00730836636693,-0.559560573777918));
#40338=CARTESIAN_POINT('Ctrl Pts',(12.4013908554088,-7.019122574986,-0.441662516279092));
#40339=CARTESIAN_POINT('Ctrl Pts',(12.397067491958,-7.0267501449702,-0.323238258334718));
#40340=CARTESIAN_POINT('Ctrl Pts',(12.3920718206831,-7.03556384585387,-0.186398348762654));
#40341=CARTESIAN_POINT('Ctrl Pts',(12.3902516338787,-7.03876210460539,-0.0492519096262223));
#40342=CARTESIAN_POINT('Ctrl Pts',(12.3916053560035,-7.03637809537437,0.0876758270660355));
#40343=CARTESIAN_POINT('Ctrl Pts',(12.3929630026023,-7.03398717484161,0.225000520654302));
#40344=CARTESIAN_POINT('Ctrl Pts',(12.3975129673672,-7.02598155019911,0.362105241912753));
#40345=CARTESIAN_POINT('Ctrl Pts',(12.4052079364272,-7.01236879050172,0.498460177595601));
#40346=CARTESIAN_POINT('Ctrl Pts',(12.4129361026925,-6.99869730339771,0.635403368116608));
#40347=CARTESIAN_POINT('Ctrl Pts',(12.4238364813948,-6.9793701376568,0.771590289741124));
#40348=CARTESIAN_POINT('Ctrl Pts',(12.4378151222668,-6.95436948862457,0.906484242526394));
#40349=CARTESIAN_POINT('Ctrl Pts',(12.4439512822523,-6.94339503240884,0.96569821639967));
#40350=CARTESIAN_POINT('Ctrl Pts',(12.4506800022041,-6.93132701813272,1.0246630456538));
#40351=CARTESIAN_POINT('Ctrl Pts',(12.4579905368414,-6.91816245718254,1.08333333333318));
#40352=CARTESIAN_POINT('Origin',(13.892722748591,-3.17092330887735,-3.20017169526122E-15));
#40353=CARTESIAN_POINT('',(15.1423033840733,-0.0114224867026808,-1.08333333333334));
#40354=CARTESIAN_POINT('',(14.6487667980729,0.141522102769127,-1.08333333333334));
#40355=CARTESIAN_POINT('Origin',(13.892722748591,-3.17092330887735,-1.08333333333334));
#40356=CARTESIAN_POINT('',(13.1366786991091,-6.48336872052383,-1.08333333333334));
#40357=CARTESIAN_POINT('Origin',(13.892722748591,-3.17092330887735,-3.20017169526122E-15));
#40358=CARTESIAN_POINT('',(13.6476999686242,-6.55970790622078,-1.08333333333334));
#40359=CARTESIAN_POINT('Origin',(13.892722748591,-3.17092330887735,-1.08333333333334));
#40360=CARTESIAN_POINT('',(13.6476999686242,-6.55970790622078,1.08333333333333));
#40361=CARTESIAN_POINT('Ctrl Pts',(13.6476999686242,-6.55970790622078,-1.08333333333334));
#40362=CARTESIAN_POINT('Ctrl Pts',(13.5948858118209,-6.66958959248674,-0.727666221822799));
#40363=CARTESIAN_POINT('Ctrl Pts',(13.5683505740919,-6.72230205711255,-0.35278297384278));
#40364=CARTESIAN_POINT('Ctrl Pts',(13.5683505740919,-6.72230205711255,-3.93962482987281E-15));
#40365=CARTESIAN_POINT('Ctrl Pts',(13.5683505740919,-6.72230205711255,0.352782973842772));
#40366=CARTESIAN_POINT('Ctrl Pts',(13.5948858118209,-6.66958959248674,0.727666221822791));
#40367=CARTESIAN_POINT('Ctrl Pts',(13.6476999686242,-6.55970790622078,1.08333333333333));
#40368=CARTESIAN_POINT('',(12.7471768669564,-6.36961395396396,1.08333333333333));
#40369=CARTESIAN_POINT('Origin',(13.892722748591,-3.17092330887735,1.08333333333333));
#40370=CARTESIAN_POINT('',(12.7471768669564,-6.36961395396396,-1.08333333333334));
#40371=CARTESIAN_POINT('Ctrl Pts',(12.7471768669564,-6.36961395396397,1.08333333333334));
#40372=CARTESIAN_POINT('Ctrl Pts',(12.6958726976266,-6.47228631765585,0.725928647976583));
#40373=CARTESIAN_POINT('Ctrl Pts',(12.6703734952067,-6.52105325020152,0.352039859176988));
#40374=CARTESIAN_POINT('Ctrl Pts',(12.6703734952067,-6.52105325020152,-3.73360976135914E-15));
#40375=CARTESIAN_POINT('Ctrl Pts',(12.6703734952067,-6.52105325020152,-0.352039859176996));
#40376=CARTESIAN_POINT('Ctrl Pts',(12.6958726976266,-6.47228631765585,-0.72592864797659));
#40377=CARTESIAN_POINT('Ctrl Pts',(12.7471768669564,-6.36961395396397,-1.08333333333335));
#40378=CARTESIAN_POINT('Origin',(13.892722748591,-3.17092330887735,-1.08333333333334));
#40379=CARTESIAN_POINT('',(14.2484814298548,0.208031110850763,-1.08333333333334));
#40380=CARTESIAN_POINT('Origin',(13.892722748591,-3.17092330887735,-1.08333333333334));
#40381=CARTESIAN_POINT('',(14.2484814298548,0.208031110850763,1.08333333333333));
#40382=CARTESIAN_POINT('Ctrl Pts',(14.2484814298548,0.208031110850765,-1.08333333333334));
#40383=CARTESIAN_POINT('Ctrl Pts',(14.2468058395578,0.322795758952199,-0.725928647976584));
#40384=CARTESIAN_POINT('Ctrl Pts',(14.2449910310593,0.377796936249431,-0.352039859176992));
#40385=CARTESIAN_POINT('Ctrl Pts',(14.2449910310593,0.37779693624943,0.352039859176986));
#40386=CARTESIAN_POINT('Ctrl Pts',(14.2468058395578,0.322795758952199,0.725928647976576));
#40387=CARTESIAN_POINT('Ctrl Pts',(14.2484814298548,0.208031110850766,1.08333333333333));
#40388=CARTESIAN_POINT('',(15.1423033840733,-0.0114224867026808,1.08333333333333));
#40389=CARTESIAN_POINT('Origin',(13.892722748591,-3.17092330887735,1.08333333333333));
#40390=CARTESIAN_POINT('Ctrl Pts',(15.1423033840733,-0.0114224867026912,
1.08333333333333));
#40391=CARTESIAN_POINT('Ctrl Pts',(15.1423953499066,0.110492695607724,0.727666221822789));
#40392=CARTESIAN_POINT('Ctrl Pts',(15.1413590080604,0.169498193350193,0.352782973842772));
#40393=CARTESIAN_POINT('Ctrl Pts',(15.1413590080604,0.169498193350193,-0.352782973842778));
#40394=CARTESIAN_POINT('Ctrl Pts',(15.1423953499066,0.110492695607724,-0.727666221822797));
#40395=CARTESIAN_POINT('Ctrl Pts',(15.1423033840733,-0.0114224867026924,
-1.08333333333334));
#40396=CARTESIAN_POINT('',(13.0227870731057,-2.97236616780865,3.45272288248773));
#40397=CARTESIAN_POINT('Origin',(13.0227870731057,-2.97236616780865,-2.9997830762867E-15));
#40398=CARTESIAN_POINT('',(14.7626584240763,-3.36948044994605,3.45272288248773));
#40399=CARTESIAN_POINT('Origin',(14.7626584240763,-3.36948044994605,-3.40056031423575E-15));
#40400=CARTESIAN_POINT('Origin',(11.1410986251693,8.88472967648709,-9.85584169237555E-16));
#40401=CARTESIAN_POINT('',(11.8387328710639,9.44107442276104,-3.96060240207311));
#40402=CARTESIAN_POINT('Origin',(11.8387328710639,9.44107442276104,-1.0472995612114E-15));
#40403=CARTESIAN_POINT('',(10.4434643792748,8.32838493021314,-3.96060240207311));
#40404=CARTESIAN_POINT('Origin',(11.1410986251693,8.88472967648709,-2.5198520116158));
#40405=CARTESIAN_POINT('Origin',(10.4434643792748,8.32838493021314,-9.23868777263706E-16));
#40406=CARTESIAN_POINT('',(8.89378902201275,12.2552029391784,1.08333333331655));
#40407=CARTESIAN_POINT('',(8.89378902201677,12.2552029391754,-1.08333333333333));
#40408=CARTESIAN_POINT('Ctrl Pts',(8.89378902201274,12.2552029391784,1.08333333331655));
#40409=CARTESIAN_POINT('Ctrl Pts',(8.86335293025879,12.2772908784853,0.956315399884826));
#40410=CARTESIAN_POINT('Ctrl Pts',(8.83824313040494,12.2953456493747,0.827586922367285));
#40411=CARTESIAN_POINT('Ctrl Pts',(8.81859777764014,12.3094197866805,0.69766772380084));
#40412=CARTESIAN_POINT('Ctrl Pts',(8.7991879276401,12.3233252073292,0.569305958731489));
#40413=CARTESIAN_POINT('Ctrl Pts',(8.78511225071473,12.3333449381983,0.439781849534452));
#40414=CARTESIAN_POINT('Ctrl Pts',(8.77647376760361,12.3394890678296,0.309596747993595));
#40415=CARTESIAN_POINT('Ctrl Pts',(8.76964787761092,12.344343988818,0.206728088024587));
#40416=CARTESIAN_POINT('Ctrl Pts',(8.76621624622163,12.3467783236357,0.103446722778746));
#40417=CARTESIAN_POINT('Ctrl Pts',(8.76621624622163,12.3467783236357,7.54951656745106E-15));
#40418=CARTESIAN_POINT('Ctrl Pts',(8.76621624622163,12.3467783236357,-0.130951008152141));
#40419=CARTESIAN_POINT('Ctrl Pts',(8.77171477448527,12.3428797767713,-0.261548325668487));
#40420=CARTESIAN_POINT('Ctrl Pts',(8.78261416841303,12.3351194002049,-0.391301356121213));
#40421=CARTESIAN_POINT('Ctrl Pts',(8.79368558213778,12.3272365454154,-0.523102215114213));
#40422=CARTESIAN_POINT('Ctrl Pts',(8.81032969837903,12.3153689336875,-0.654031926803563));
#40423=CARTESIAN_POINT('Ctrl Pts',(8.83241243050519,12.2995110840219,-0.783576297698762));
#40424=CARTESIAN_POINT('Ctrl Pts',(8.84960195907419,12.2871670969504,-0.88441557119687));
#40425=CARTESIAN_POINT('Ctrl Pts',(8.87008627043973,12.2724043900869,-0.984415425401903));
#40426=CARTESIAN_POINT('Ctrl Pts',(8.89378902201675,12.2552029391755,-1.08333333333333));
#40427=CARTESIAN_POINT('',(8.22258343557175,11.6383685130288,1.08333333333333));
#40428=CARTESIAN_POINT('Ctrl Pts',(8.89378902201473,12.2552029391744,1.08333333333333));
#40429=CARTESIAN_POINT('Ctrl Pts',(8.7875190745609,12.202353722575,1.08333333333333));
#40430=CARTESIAN_POINT('Ctrl Pts',(8.68681488082435,12.1369760343753,1.08333333333333));
#40431=CARTESIAN_POINT('Ctrl Pts',(8.46069343470619,11.9566501984405,1.08333333333333));
#40432=CARTESIAN_POINT('Ctrl Pts',(8.31988542322913,11.7983921800676,1.08333333333333));
#40433=CARTESIAN_POINT('Ctrl Pts',(8.22258343557172,11.6383685130288,1.08333333333333));
#40434=CARTESIAN_POINT('',(8.22258343557123,11.6383685130292,-1.08333333333333));
#40435=CARTESIAN_POINT('Ctrl Pts',(8.2225834355717,11.6383685130289,-1.08333333333318));
#40436=CARTESIAN_POINT('Ctrl Pts',(8.19448780675769,11.6582182584498,-0.949301954017324));
#40437=CARTESIAN_POINT('Ctrl Pts',(8.17159767874311,11.6742430454627,-0.81366496302888));
#40438=CARTESIAN_POINT('Ctrl Pts',(8.15402161030241,11.6865063889394,-0.67695567866062));
#40439=CARTESIAN_POINT('Ctrl Pts',(8.13658119548769,11.6986750828637,-0.541301528447691));
#40440=CARTESIAN_POINT('Ctrl Pts',(8.12437307855494,11.7071402381473,-0.40459157308691));
#40441=CARTESIAN_POINT('Ctrl Pts',(8.1174733585697,11.7119223986889,-0.26734687734235));
#40442=CARTESIAN_POINT('Ctrl Pts',(8.11300215046573,11.7150213700985,-0.178408544025479));
#40443=CARTESIAN_POINT('Ctrl Pts',(8.11075954642938,11.7165728598428,-0.0892456520429063));
#40444=CARTESIAN_POINT('Ctrl Pts',(8.11075954642938,11.7165728598428,1.33226762955019E-15));
#40445=CARTESIAN_POINT('Ctrl Pts',(8.11075954642938,11.7165728598428,0.137335411050026));
#40446=CARTESIAN_POINT('Ctrl Pts',(8.11607262981309,11.7129002012938,0.274553571737022));
#40447=CARTESIAN_POINT('Ctrl Pts',(8.12665801674411,11.7055512249056,0.411127959090392));
#40448=CARTESIAN_POINT('Ctrl Pts',(8.13729388250879,11.698167203246,0.548353632582512));
#40449=CARTESIAN_POINT('Ctrl Pts',(8.15325248641432,11.6870716767896,0.684929378140945));
#40450=CARTESIAN_POINT('Ctrl Pts',(8.17446212457132,11.6722178258439,0.820321104282498));
#40451=CARTESIAN_POINT('Ctrl Pts',(8.18828255682692,11.6625388940673,0.908543834215877));
#40452=CARTESIAN_POINT('Ctrl Pts',(8.20433194575505,11.6512633098961,0.9962638332735));
#40453=CARTESIAN_POINT('Ctrl Pts',(8.22258343557176,11.6383685130288,1.08333333333334));
#40454=CARTESIAN_POINT('Ctrl Pts',(8.89378902201675,12.2552029391755,-1.08333333333333));
#40455=CARTESIAN_POINT('Ctrl Pts',(8.78751907456219,12.2023537225759,-1.08333333333333));
#40456=CARTESIAN_POINT('Ctrl Pts',(8.68681488082489,12.1369760343758,-1.08333333333333));
#40457=CARTESIAN_POINT('Ctrl Pts',(8.46069343470621,11.9566501984405,-1.08333333333333));
#40458=CARTESIAN_POINT('Ctrl Pts',(8.31988542322917,11.7983921800676,-1.08333333333333));
#40459=CARTESIAN_POINT('Ctrl Pts',(8.22258343557176,11.6383685130289,-1.08333333333333));
#40460=CARTESIAN_POINT('',(13.9269936544443,5.94376395877129,1.08333333333333));
#40461=CARTESIAN_POINT('',(13.1762672612271,5.42664547033562,1.08333333333333));
#40462=CARTESIAN_POINT('Ctrl Pts',(13.9269936544443,5.94376395877129,1.08333333333333));
#40463=CARTESIAN_POINT('Ctrl Pts',(13.8517896638478,5.85187873682469,1.08333333333333));
#40464=CARTESIAN_POINT('Ctrl Pts',(13.7657237213495,5.76832601371371,1.08333333333333));
#40465=CARTESIAN_POINT('Ctrl Pts',(13.5395781511316,5.5879809394513,1.08333333333333));
#40466=CARTESIAN_POINT('Ctrl Pts',(13.3544742809805,5.48608062863226,1.08333333333333));
#40467=CARTESIAN_POINT('Ctrl Pts',(13.1762672612269,5.42664547033621,1.08333333333333));
#40468=CARTESIAN_POINT('',(13.9269936544443,5.94376395877129,-1.08333333333333));
#40469=CARTESIAN_POINT('Ctrl Pts',(13.9269936544443,5.9437639587713,1.08333333333333));
#40470=CARTESIAN_POINT('Ctrl Pts',(13.9416885168395,5.90933203032488,0.95688863210334));
#40471=CARTESIAN_POINT('Ctrl Pts',(13.9536527109305,5.88095561854266,0.828820583351241));
#40472=CARTESIAN_POINT('Ctrl Pts',(13.9629765258053,5.85873440158633,0.699646919261855));
#40473=CARTESIAN_POINT('Ctrl Pts',(13.9722513158077,5.83663002439342,0.571152453813261));
#40474=CARTESIAN_POINT('Ctrl Pts',(13.9789135007645,5.82061622745854,0.441563969171658));
#40475=CARTESIAN_POINT('Ctrl Pts',(13.9830050237944,5.81077040959811,0.31139107363785));
#40476=CARTESIAN_POINT('Ctrl Pts',(13.987063711968,5.80100360535004,0.182262827807452));
#40477=CARTESIAN_POINT('Ctrl Pts',(13.9885928700522,5.79730615639857,0.0525595133520559));
#40478=CARTESIAN_POINT('Ctrl Pts',(13.9875862925321,5.79973378332923,-0.077221432194654));
#40479=CARTESIAN_POINT('Ctrl Pts',(13.9868997670033,5.80138952054645,-0.165737150534494));
#40480=CARTESIAN_POINT('Ctrl Pts',(13.9850326975557,5.80589410253397,-0.254288981130278));
#40481=CARTESIAN_POINT('Ctrl Pts',(13.9819702480148,5.81325986277498,-0.342719102199545));
#40482=CARTESIAN_POINT('Ctrl Pts',(13.977353348451,5.82436436418423,-0.476034927301432));
#40483=CARTESIAN_POINT('Ctrl Pts',(13.9700489046451,5.84190742581571,-0.608312350205104));
#40484=CARTESIAN_POINT('Ctrl Pts',(13.9600480872369,5.86570879353505,-0.739057191236667));
#40485=CARTESIAN_POINT('Ctrl Pts',(13.9511688384277,5.88684089277784,-0.855139299993628));
#40486=CARTESIAN_POINT('Ctrl Pts',(13.9401632237805,5.91290598563348,-0.970013302477476));
#40487=CARTESIAN_POINT('Ctrl Pts',(13.9269936544443,5.9437639587713,-1.08333333333333));
#40488=CARTESIAN_POINT('',(13.1762672612355,5.42664547033908,-1.08333333333333));
#40489=CARTESIAN_POINT('Ctrl Pts',(13.9269936544443,5.94376395877129,-1.08333333333333));
#40490=CARTESIAN_POINT('Ctrl Pts',(13.8517896638478,5.85187873682469,-1.08333333333333));
#40491=CARTESIAN_POINT('Ctrl Pts',(13.7657237213495,5.76832601371371,-1.08333333333333));
#40492=CARTESIAN_POINT('Ctrl Pts',(13.5395781511339,5.5879809394531,-1.08333333333333));
#40493=CARTESIAN_POINT('Ctrl Pts',(13.3544742809865,5.48608062863536,-1.08333333333333));
#40494=CARTESIAN_POINT('Ctrl Pts',(13.1762672612355,5.42664547033908,-1.08333333333333));
#40495=CARTESIAN_POINT('Ctrl Pts',(13.1762672612269,5.42664547033617,-1.08333333333318));
#40496=CARTESIAN_POINT('Ctrl Pts',(13.1893705593041,5.39482976422236,-0.949270311030452));
#40497=CARTESIAN_POINT('Ctrl Pts',(13.1999097963792,5.36892368585892,-0.813521288368082));
#40498=CARTESIAN_POINT('Ctrl Pts',(13.2079621630868,5.34904061477083,-0.676607052101254));
#40499=CARTESIAN_POINT('Ctrl Pts',(13.2148460430323,5.33204279546023,-0.559560573777983));
#40500=CARTESIAN_POINT('Ctrl Pts',(13.2199117356377,5.31944645364959,-0.441662516279123));
#40501=CARTESIAN_POINT('Ctrl Pts',(13.2231796369647,5.31131059989547,-0.323238258334714));
#40502=CARTESIAN_POINT('Ctrl Pts',(13.2269557156993,5.30190957419912,-0.186398348762647));
#40503=CARTESIAN_POINT('Ctrl Pts',(13.2283213471703,5.2984924131362,-0.0492519096262126));
#40504=CARTESIAN_POINT('Ctrl Pts',(13.2273014856384,5.30103720115497,0.087675827066048));
#40505=CARTESIAN_POINT('Ctrl Pts',(13.2262786675026,5.30358936657715,0.225000520654307));
#40506=CARTESIAN_POINT('Ctrl Pts',(13.22285647475,5.31213809759657,0.362105241912749));
#40507=CARTESIAN_POINT('Ctrl Pts',(13.2170113253899,5.32664168351083,0.498460177595588));
#40508=CARTESIAN_POINT('Ctrl Pts',(13.2111409592133,5.34120783998435,0.635403368116607));
#40509=CARTESIAN_POINT('Ctrl Pts',(13.2028266475275,5.36178038996296,0.771590289741134));
#40510=CARTESIAN_POINT('Ctrl Pts',(13.1919958930594,5.38829698119018,0.906484242526414));
#40511=CARTESIAN_POINT('Ctrl Pts',(13.1872415508606,5.3999368857798,0.965698216399684));
#40512=CARTESIAN_POINT('Ctrl Pts',(13.1820016856381,5.41272189470467,1.02466304565381));
#40513=CARTESIAN_POINT('Ctrl Pts',(13.1762672612269,5.42664547033617,1.08333333333318));
#40514=CARTESIAN_POINT('Origin',(11.1410986251693,8.88472967648709,-9.85584169237555E-16));
#40515=CARTESIAN_POINT('',(8.72113759169208,11.2696166353064,-1.08333333333333));
#40516=CARTESIAN_POINT('',(9.02271027299523,11.54110464988,-1.08333333333333));
#40517=CARTESIAN_POINT('Origin',(11.1410986251693,8.88472967648709,-1.08333333333333));
#40518=CARTESIAN_POINT('',(8.72113759169208,11.2696166353064,1.08333333333333));
#40519=CARTESIAN_POINT('Ctrl Pts',(8.72113759169207,11.2696166353064,1.08333333333334));
#40520=CARTESIAN_POINT('Ctrl Pts',(8.63036626326973,11.3398611937657,0.725928647976583));
#40521=CARTESIAN_POINT('Ctrl Pts',(8.5862330966948,11.3727349924819,0.35203985917699));
#40522=CARTESIAN_POINT('Ctrl Pts',(8.5862330966948,11.3727349924819,-0.352039859176991));
#40523=CARTESIAN_POINT('Ctrl Pts',(8.63036626326973,11.3398611937657,-0.725928647976582));
#40524=CARTESIAN_POINT('Ctrl Pts',(8.72113759169207,11.2696166353064,-1.08333333333334));
#40525=CARTESIAN_POINT('',(9.4500021963329,11.8316076987797,1.08333333333333));
#40526=CARTESIAN_POINT('Origin',(11.1410986251693,8.88472967648709,1.08333333333333));
#40527=CARTESIAN_POINT('',(9.4500021963329,11.8316076987797,-1.08333333333333));
#40528=CARTESIAN_POINT('Ctrl Pts',(9.4500021963329,11.8316076987798,-1.08333333333334));
#40529=CARTESIAN_POINT('Ctrl Pts',(9.35474240837097,11.9076924734258,-0.7276662218228));
#40530=CARTESIAN_POINT('Ctrl Pts',(9.30796390402485,11.9436715548399,-0.352782973842779));
#40531=CARTESIAN_POINT('Ctrl Pts',(9.30796390402485,11.9436715548399,0.352782973842777));
#40532=CARTESIAN_POINT('Ctrl Pts',(9.35474240837097,11.9076924734258,0.727666221822799));
#40533=CARTESIAN_POINT('Ctrl Pts',(9.4500021963329,11.8316076987798,1.08333333333334));
#40534=CARTESIAN_POINT('Origin',(11.1410986251693,8.88472967648709,-1.08333333333333));
#40535=CARTESIAN_POINT('',(13.2594869773434,6.22835470309422,-1.08333333333333));
#40536=CARTESIAN_POINT('Origin',(11.1410986251693,8.88472967648709,-9.85584169237555E-16));
#40537=CARTESIAN_POINT('',(13.6377879061428,6.58029051604763,-1.08333333333333));
#40538=CARTESIAN_POINT('Origin',(11.1410986251693,8.88472967648709,-1.08333333333333));
#40539=CARTESIAN_POINT('',(13.6377879061428,6.58029051604763,1.08333333333333));
#40540=CARTESIAN_POINT('Ctrl Pts',(13.6377879061428,6.58029051604764,-1.08333333333332));
#40541=CARTESIAN_POINT('Ctrl Pts',(13.6907677796515,6.47048863474093,-0.727666221822788));
#40542=CARTESIAN_POINT('Ctrl Pts',(13.7154355939006,6.41687686636464,-0.352782973842773));
#40543=CARTESIAN_POINT('Ctrl Pts',(13.7154355939006,6.41687686636464,-9.86054494281319E-16));
#40544=CARTESIAN_POINT('Ctrl Pts',(13.7154355939006,6.41687686636464,0.352782973842772));
#40545=CARTESIAN_POINT('Ctrl Pts',(13.6907677796515,6.47048863474094,0.727666221822788));
#40546=CARTESIAN_POINT('Ctrl Pts',(13.6377879061428,6.58029051604764,1.08333333333332));
#40547=CARTESIAN_POINT('',(12.9276994994135,5.9947548451011,1.08333333333333));
#40548=CARTESIAN_POINT('Origin',(11.1410986251693,8.88472967648709,1.08333333333333));
#40549=CARTESIAN_POINT('',(12.9276994994135,5.9947548451011,-1.08333333333333));
#40550=CARTESIAN_POINT('Ctrl Pts',(12.9276994994135,5.9947548451011,1.08333333333333));
#40551=CARTESIAN_POINT('Ctrl Pts',(12.9759843593573,5.89062845864264,0.72592864797658));
#40552=CARTESIAN_POINT('Ctrl Pts',(12.9982133898606,5.84028669430273,0.352039859176989));
#40553=CARTESIAN_POINT('Ctrl Pts',(12.9982133898606,5.84028669430273,-9.85141416048961E-16));
#40554=CARTESIAN_POINT('Ctrl Pts',(12.9982133898606,5.84028669430273,-0.35203985917699));
#40555=CARTESIAN_POINT('Ctrl Pts',(12.9759843593573,5.89062845864264,-0.72592864797658));
#40556=CARTESIAN_POINT('Ctrl Pts',(12.9276994994135,5.9947548451011,-1.08333333333333));
#40557=CARTESIAN_POINT('Origin',(11.1410986251693,8.88472967648709,-1.08333333333333));
#40558=CARTESIAN_POINT('',(10.4434643792748,8.32838493021314,3.45272288248773));
#40559=CARTESIAN_POINT('Origin',(10.4434643792748,8.32838493021314,-9.23868777263706E-16));
#40560=CARTESIAN_POINT('',(11.8387328710639,9.44107442276105,3.45272288248773));
#40561=CARTESIAN_POINT('Origin',(11.8387328710639,9.44107442276104,-1.0472995612114E-15));
#40562=CARTESIAN_POINT('Origin',(0.,14.25,0.));
#40563=CARTESIAN_POINT('',(-3.35834339016074,14.7651959662676,-1.08333333333333));
#40564=CARTESIAN_POINT('',(-3.39763111739558,14.25,-1.08333333333333));
#40565=CARTESIAN_POINT('Origin',(1.55588456152529E-16,14.25,-1.08333333333333));
#40566=CARTESIAN_POINT('',(3.39763111739558,14.25,-1.08333333333333));
#40567=CARTESIAN_POINT('Origin',(0.,14.25,0.));
#40568=CARTESIAN_POINT('',(3.35834339016074,14.7651959662676,-1.08333333333333));
#40569=CARTESIAN_POINT('Origin',(0.,14.25,-1.08333333333333));
#40570=CARTESIAN_POINT('',(3.35834339016074,14.7651959662676,1.08333333333333));
#40571=CARTESIAN_POINT('Ctrl Pts',(3.35834339016074,14.7651959662676,-1.08333333333333));
#40572=CARTESIAN_POINT('Ctrl Pts',(3.47722236863702,14.7381569460943,-0.727666221822793));
#40573=CARTESIAN_POINT('Ctrl Pts',(3.53451786760282,14.7240166290356,-0.352782973842775));
#40574=CARTESIAN_POINT('Ctrl Pts',(3.53451786760282,14.7240166290356,0.));
#40575=CARTESIAN_POINT('Ctrl Pts',(3.53451786760282,14.7240166290356,0.352782973842776));
#40576=CARTESIAN_POINT('Ctrl Pts',(3.47722236863702,14.7381569460943,0.727666221822795));
#40577=CARTESIAN_POINT('Ctrl Pts',(3.35834339016074,14.7651959662676,1.08333333333333));
#40578=CARTESIAN_POINT('',(3.37340073180097,13.8449509750914,1.08333333333333));
#40579=CARTESIAN_POINT('Origin',(0.,14.25,1.08333333333333));
#40580=CARTESIAN_POINT('',(3.37340073180097,13.8449509750914,-1.08333333333333));
#40581=CARTESIAN_POINT('Ctrl Pts',(3.37340073180098,13.8449509750914,1.08333333333333));
#40582=CARTESIAN_POINT('Ctrl Pts',(3.48491513664897,13.8177798586608,0.725928647976577));
#40583=CARTESIAN_POINT('Ctrl Pts',(3.53813348671686,13.8037716378594,0.352039859176988));
#40584=CARTESIAN_POINT('Ctrl Pts',(3.53813348671686,13.8037716378594,0.));
#40585=CARTESIAN_POINT('Ctrl Pts',(3.53813348671686,13.8037716378594,-0.352039859176988));
#40586=CARTESIAN_POINT('Ctrl Pts',(3.48491513664897,13.8177798586608,-0.725928647976578));
#40587=CARTESIAN_POINT('Ctrl Pts',(3.37340073180098,13.8449509750914,-1.08333333333333));
#40588=CARTESIAN_POINT('Origin',(0.,14.25,-1.08333333333333));
#40589=CARTESIAN_POINT('',(-3.37340073180097,13.8449509750914,-1.08333333333333));
#40590=CARTESIAN_POINT('Origin',(1.55588456152529E-16,14.25,-1.08333333333333));
#40591=CARTESIAN_POINT('',(-3.37340073180097,13.8449509750914,1.08333333333333));
#40592=CARTESIAN_POINT('Ctrl Pts',(-3.37340073180098,13.8449509750914,-1.08333333333333));
#40593=CARTESIAN_POINT('Ctrl Pts',(-3.48491513664897,13.8177798586608,-0.725928647976578));
#40594=CARTESIAN_POINT('Ctrl Pts',(-3.53813348671686,13.8037716378594,-0.352039859176988));
#40595=CARTESIAN_POINT('Ctrl Pts',(-3.53813348671686,13.8037716378594,0.352039859176988));
#40596=CARTESIAN_POINT('Ctrl Pts',(-3.48491513664897,13.8177798586608,0.725928647976578));
#40597=CARTESIAN_POINT('Ctrl Pts',(-3.37340073180098,13.8449509750914,1.08333333333333));
#40598=CARTESIAN_POINT('',(-3.35834339016074,14.7651959662676,1.08333333333333));
#40599=CARTESIAN_POINT('Origin',(-1.5558845615253E-16,14.25,1.08333333333333));
#40600=CARTESIAN_POINT('Ctrl Pts',(-3.35834339016074,14.7651959662676,1.08333333333333));
#40601=CARTESIAN_POINT('Ctrl Pts',(-3.47722236863702,14.7381569460943,0.727666221822794));
#40602=CARTESIAN_POINT('Ctrl Pts',(-3.53451786760282,14.7240166290356,0.352782973842775));
#40603=CARTESIAN_POINT('Ctrl Pts',(-3.53451786760282,14.7240166290356,-0.352782973842776));
#40604=CARTESIAN_POINT('Ctrl Pts',(-3.47722236863702,14.7381569460943,-0.727666221822794));
#40605=CARTESIAN_POINT('Ctrl Pts',(-3.35834339016074,14.7651959662676,-1.08333333333333));
#40606=CARTESIAN_POINT('',(0.,13.3576923076923,3.45272288248773));
#40607=CARTESIAN_POINT('Origin',(0.,13.3576923076923,0.));
#40608=CARTESIAN_POINT('',(0.,15.1423076923077,3.45272288248773));
#40609=CARTESIAN_POINT('Origin',(0.,15.1423076923077,0.));
#40610=CARTESIAN_POINT('Origin',(0.,14.25,0.));
#40611=CARTESIAN_POINT('',(-4.85033905439415E-16,15.1423076923077,-3.96060240207311));
#40612=CARTESIAN_POINT('Origin',(0.,15.1423076923077,0.));
#40613=CARTESIAN_POINT('',(-4.85033905439415E-16,13.3576923076923,-3.96060240207311));
#40614=CARTESIAN_POINT('Origin',(-3.08592870035031E-16,14.25,-2.5198520116158));
#40615=CARTESIAN_POINT('Origin',(0.,13.3576923076923,0.));
#40616=CARTESIAN_POINT('',(-3.97254599103887,13.6850786752975,1.08333333333333));
#40617=CARTESIAN_POINT('',(-4.03631672677061,14.5944383081266,1.08333333333333));
#40618=CARTESIAN_POINT('Ctrl Pts',(-3.97254599103889,13.6850786752975,1.08333333333333));
#40619=CARTESIAN_POINT('Ctrl Pts',(-4.03699073486477,13.8609255570095,1.08333333333333));
#40620=CARTESIAN_POINT('Ctrl Pts',(-4.07292947680577,14.0696859538838,1.08333333333333));
#40621=CARTESIAN_POINT('Ctrl Pts',(-4.07292947680577,14.358906139038,1.08333333333333));
#40622=CARTESIAN_POINT('Ctrl Pts',(-4.06125577389194,14.4784021699804,1.08333333333333));
#40623=CARTESIAN_POINT('Ctrl Pts',(-4.03631672677123,14.5944383081267,1.08333333333333));
#40624=CARTESIAN_POINT('',(-3.97254599103887,13.6850786752975,-1.08333333333333));
#40625=CARTESIAN_POINT('Ctrl Pts',(-3.97254599103885,13.6850786752975,1.08333333333333));
#40626=CARTESIAN_POINT('Ctrl Pts',(-4.0055902844374,13.6754864779574,0.949270311030653));
#40627=CARTESIAN_POINT('Ctrl Pts',(-4.03241557892495,13.6675742096383,0.813521288368336));
#40628=CARTESIAN_POINT('Ctrl Pts',(-4.05298135839275,13.6614729113855,0.67660705210156));
#40629=CARTESIAN_POINT('Ctrl Pts',(-4.07056281760631,13.6562569784544,0.559560573778188));
#40630=CARTESIAN_POINT('Ctrl Pts',(-4.08356944187665,13.6523638057542,0.441662516279225));
#40631=CARTESIAN_POINT('Ctrl Pts',(-4.09196781162929,13.6498461320482,0.32323825833471));
#40632=CARTESIAN_POINT('Ctrl Pts',(-4.10167217606822,13.6469369456345,0.186398348762652));
#40633=CARTESIAN_POINT('Ctrl Pts',(-4.10519527746315,13.6458740742379,0.0492519096262281));
#40634=CARTESIAN_POINT('Ctrl Pts',(-4.1025698088094,13.6466633637621,-0.0876758270660229));
#40635=CARTESIAN_POINT('Ctrl Pts',(-4.09993672885708,13.6474549414561,-0.225000520654293));
#40636=CARTESIAN_POINT('Ctrl Pts',(-4.0911193595297,13.6501094100325,-0.362105241912746));
#40637=CARTESIAN_POINT('Ctrl Pts',(-4.07613560843688,13.6545823261509,-0.498460177595596));
#40638=CARTESIAN_POINT('Ctrl Pts',(-4.06108721528303,13.659074539074,-0.635403368116582));
#40639=CARTESIAN_POINT('Ctrl Pts',(-4.03981905948952,13.6654009235528,-0.771590289741077));
#40640=CARTESIAN_POINT('Ctrl Pts',(-4.01233468870309,13.673465922941,-0.906484242526326));
#40641=CARTESIAN_POINT('Ctrl Pts',(-4.00026996096645,13.6770061903378,-0.965698216399675));
#40642=CARTESIAN_POINT('Ctrl Pts',(-3.98700723595603,13.6808808214243,-1.02466304565388));
#40643=CARTESIAN_POINT('Ctrl Pts',(-3.97254599103885,13.6850786752975,-1.08333333333333));
#40644=CARTESIAN_POINT('',(-4.03631672677098,14.5944383081279,-1.08333333333333));
#40645=CARTESIAN_POINT('Ctrl Pts',(-3.97254599103889,13.6850786752975,-1.08333333333333));
#40646=CARTESIAN_POINT('Ctrl Pts',(-4.03718797255354,13.8614637488071,-1.08333333333333));
#40647=CARTESIAN_POINT('Ctrl Pts',(-4.07292947680577,14.0697175866198,-1.08333333333333));
#40648=CARTESIAN_POINT('Ctrl Pts',(-4.07292947680577,14.3589686276554,-1.08333333333333));
#40649=CARTESIAN_POINT('Ctrl Pts',(-4.06126656486658,14.4783519618466,-1.08333333333333));
#40650=CARTESIAN_POINT('Ctrl Pts',(-4.03631672677098,14.5944383081279,-1.08333333333333));
#40651=CARTESIAN_POINT('Ctrl Pts',(-4.03631672677125,14.5944383081264,-1.08333333333353));
#40652=CARTESIAN_POINT('Ctrl Pts',(-4.07239878927587,14.5844592579328,-0.956888632103535));
#40653=CARTESIAN_POINT('Ctrl Pts',(-4.10204391436992,14.576120838176,-0.828820583351431));
#40654=CARTESIAN_POINT('Ctrl Pts',(-4.12523046485396,14.5695557880246,-0.699646919262042));
#40655=CARTESIAN_POINT('Ctrl Pts',(-4.14829509982461,14.5630252570856,-0.571152453813459));
#40656=CARTESIAN_POINT('Ctrl Pts',(-4.16496899480084,14.5582495239489,-0.441563969171867));
#40657=CARTESIAN_POINT('Ctrl Pts',(-4.17521778805797,14.555309638438,-0.311391073638072));
#40658=CARTESIAN_POINT('Ctrl Pts',(-4.18538433378736,14.5523933457842,-0.182262827807668));
#40659=CARTESIAN_POINT('Ctrl Pts',(-4.18922853025337,14.5512835680019,-0.0525595133522669));
#40660=CARTESIAN_POINT('Ctrl Pts',(-4.18670294427272,14.5520101946411,0.0772214321944475));
#40661=CARTESIAN_POINT('Ctrl Pts',(-4.18498039512374,14.5525057826387,0.165737150534356));
#40662=CARTESIAN_POINT('Ctrl Pts',(-4.1802944723506,14.5538546098955,0.254288981130209));
#40663=CARTESIAN_POINT('Ctrl Pts',(-4.17262628304436,14.5560527668241,0.342719102199544));
#40664=CARTESIAN_POINT('Ctrl Pts',(-4.16106584445129,14.5593666727772,0.476034927301542));
#40665=CARTESIAN_POINT('Ctrl Pts',(-4.14279588034764,14.5645937486684,0.608312350205319));
#40666=CARTESIAN_POINT('Ctrl Pts',(-4.11795181407459,14.5716147048116,0.739057191236983));
#40667=CARTESIAN_POINT('Ctrl Pts',(-4.09589395251526,14.5778482769217,0.855139299993905));
#40668=CARTESIAN_POINT('Ctrl Pts',(-4.06865355383155,14.5854950604866,0.970013302477714));
#40669=CARTESIAN_POINT('Ctrl Pts',(-4.03631672677125,14.5944383081264,1.08333333333353));
#40670=CARTESIAN_POINT('',(4.0363167267713,14.5944383081264,1.08333333333333));
#40671=CARTESIAN_POINT('',(3.97254599103947,13.6850786752973,1.08333333333333));
#40672=CARTESIAN_POINT('Ctrl Pts',(4.0363167267713,14.5944383081264,1.08333333333333));
#40673=CARTESIAN_POINT('Ctrl Pts',(4.06125577389196,14.4784021699801,1.08333333333333));
#40674=CARTESIAN_POINT('Ctrl Pts',(4.07292947680577,14.3589061390379,1.08333333333333));
#40675=CARTESIAN_POINT('Ctrl Pts',(4.07292947680577,14.0696859538838,1.08333333333333));
#40676=CARTESIAN_POINT('Ctrl Pts',(4.03699073486477,13.8609255570095,1.08333333333333));
#40677=CARTESIAN_POINT('Ctrl Pts',(3.97254599103889,13.6850786752975,1.08333333333333));
#40678=CARTESIAN_POINT('',(4.0363167267713,14.5944383081264,-1.08333333333333));
#40679=CARTESIAN_POINT('Ctrl Pts',(4.0363167267713,14.5944383081264,1.08333333333333));
#40680=CARTESIAN_POINT('Ctrl Pts',(4.07267660468553,14.5843824238018,0.955915065626592));
#40681=CARTESIAN_POINT('Ctrl Pts',(4.10254364280131,14.5759803979714,0.826701571450557));
#40682=CARTESIAN_POINT('Ctrl Pts',(4.12584816889326,14.5693808768856,0.696211209492171));
#40683=CARTESIAN_POINT('Ctrl Pts',(4.14878536602558,14.5628853783063,0.567777653525462));
#40684=CARTESIAN_POINT('Ctrl Pts',(4.16536539316191,14.5581360328796,0.438107164856169));
#40685=CARTESIAN_POINT('Ctrl Pts',(4.17550906341001,14.5552260824043,0.307693975181436));
#40686=CARTESIAN_POINT('Ctrl Pts',(4.18345734283739,14.55294593144,0.205506064179161));
#40687=CARTESIAN_POINT('Ctrl Pts',(4.18745357006455,14.5517942140162,0.102862147740973));
#40688=CARTESIAN_POINT('Ctrl Pts',(4.18745357006455,14.5517942140162,-4.44089209850063E-16));
#40689=CARTESIAN_POINT('Ctrl Pts',(4.18745357006455,14.5517942140162,-0.13066680730557));
#40690=CARTESIAN_POINT('Ctrl Pts',(4.18100368362964,14.5536548201376,-0.261069786498731));
#40691=CARTESIAN_POINT('Ctrl Pts',(4.16817103415993,14.5573291670729,-0.390710450871123));
#40692=CARTESIAN_POINT('Ctrl Pts',(4.15518429935153,14.561047632956,-0.521907748246283));
#40693=CARTESIAN_POINT('Ctrl Pts',(4.13566054561854,14.5666236366129,-0.652324314224272));
#40694=CARTESIAN_POINT('Ctrl Pts',(4.10965488440249,14.5739568744946,-0.781443489202978));
#40695=CARTESIAN_POINT('Ctrl Pts',(4.08920880779353,14.5797223861759,-0.882959098491578));
#40696=CARTESIAN_POINT('Ctrl Pts',(4.06475571708163,14.586573067282,-0.983672743459539));
#40697=CARTESIAN_POINT('Ctrl Pts',(4.0363167267713,14.5944383081264,-1.08333333333333));
#40698=CARTESIAN_POINT('',(3.972545991042,13.685078675306,-1.08333333333333));
#40699=CARTESIAN_POINT('Ctrl Pts',(4.0363167267713,14.5944383081264,-1.08333333333333));
#40700=CARTESIAN_POINT('Ctrl Pts',(4.06125577389196,14.4784021699801,-1.08333333333333));
#40701=CARTESIAN_POINT('Ctrl Pts',(4.07292947680577,14.3589061390379,-1.08333333333333));
#40702=CARTESIAN_POINT('Ctrl Pts',(4.07292947680577,14.0696859538867,-1.08333333333333));
#40703=CARTESIAN_POINT('Ctrl Pts',(4.03699073486612,13.8609255570161,-1.08333333333333));
#40704=CARTESIAN_POINT('Ctrl Pts',(3.97254599104201,13.685078675306,-1.08333333333333));
#40705=CARTESIAN_POINT('Ctrl Pts',(3.97254599103891,13.6850786752974,-1.08333333333318));
#40706=CARTESIAN_POINT('Ctrl Pts',(4.00550358468898,13.6755116454224,-0.949622058007565));
#40707=CARTESIAN_POINT('Ctrl Pts',(4.03223833992508,13.667626413385,-0.814376693553222));
#40708=CARTESIAN_POINT('Ctrl Pts',(4.05275116551691,13.6615412011384,-0.678132403728152));
#40709=CARTESIAN_POINT('Ctrl Pts',(4.07316650047532,13.6554849098804,-0.542535637670838));
#40710=CARTESIAN_POINT('Ctrl Pts',(4.0874189867075,13.6512115628239,-0.40594941879892));
#40711=CARTESIAN_POINT('Ctrl Pts',(4.09549564973878,13.6487880554638,-0.268901316711817));
#40712=CARTESIAN_POINT('Ctrl Pts',(4.10076932144717,13.6472056219574,-0.179415511018788));
#40713=CARTESIAN_POINT('Ctrl Pts',(4.10340966592831,13.6464108509735,-0.0897327832366672));
#40714=CARTESIAN_POINT('Ctrl Pts',(4.10340966592831,13.6464108509735,4.66293670342566E-15));
#40715=CARTESIAN_POINT('Ctrl Pts',(4.10340966592831,13.6464108509735,0.137573936980382));
#40716=CARTESIAN_POINT('Ctrl Pts',(4.09720533291532,13.6482810316174,0.274951212619736));
#40717=CARTESIAN_POINT('Ctrl Pts',(4.08483748845152,13.6519816397819,0.41161240621476));
#40718=CARTESIAN_POINT('Ctrl Pts',(4.07237395114171,13.6557108803995,0.549330978772818));
#40719=CARTESIAN_POINT('Ctrl Pts',(4.05365110225785,13.6612989721827,0.686322345436846));
#40720=CARTESIAN_POINT('Ctrl Pts',(4.02869583028489,13.6686542829587,0.822054935347102));
#40721=CARTESIAN_POINT('Ctrl Pts',(4.01257796374822,13.6734048590114,0.909720570537157));
#40722=CARTESIAN_POINT('Ctrl Pts',(3.99385994844905,13.6788915953345,0.996861109122728));
#40723=CARTESIAN_POINT('Ctrl Pts',(3.97254599103891,13.6850786752974,1.08333333333318));
#40724=CARTESIAN_POINT('Origin',(0.,0.,1.08333333333333));
#40725=CARTESIAN_POINT('Origin',(0.,0.,-1.08333333333333));
#40726=CARTESIAN_POINT('Origin',(0.,0.,1.08333333333333));
#40727=CARTESIAN_POINT('Origin',(0.,0.,1.08333333333333));
#40728=CARTESIAN_POINT('Origin',(0.,0.,1.08333333333333));
#40729=CARTESIAN_POINT('Origin',(0.,0.,-1.08333333333333));
#40730=CARTESIAN_POINT('Origin',(0.,0.,1.08333333333333));
#40731=CARTESIAN_POINT('Origin',(0.,0.,-1.08333333333333));
#40732=CARTESIAN_POINT('Origin',(0.,15.1423076923077,3.45272288248773));
#40733=CARTESIAN_POINT('Origin',(0.,13.3576923076923,3.45272288248773));
#40734=CARTESIAN_POINT('Origin',(0.,0.,1.08333333333333));
#40735=CARTESIAN_POINT('Origin',(0.,0.,1.08333333333333));
#40736=CARTESIAN_POINT('Origin',(0.,0.,1.08333333333333));
#40737=CARTESIAN_POINT('Origin',(0.,0.,-1.08333333333333));
#40738=CARTESIAN_POINT('Origin',(0.,0.,-1.08333333333333));
#40739=CARTESIAN_POINT('Origin',(0.,0.,-1.08333333333333));
#40740=CARTESIAN_POINT('Origin',(0.,0.,1.08333333333333));
#40741=CARTESIAN_POINT('Origin',(0.,0.,1.08333333333333));
#40742=CARTESIAN_POINT('Origin',(10.4434643792748,8.32838493021314,3.45272288248773));
#40743=CARTESIAN_POINT('Origin',(11.8387328710639,9.44107442276104,3.45272288248773));
#40744=CARTESIAN_POINT('Origin',(-1.55588456152528E-16,7.49274514625042E-17,
-1.08333333333333));
#40745=CARTESIAN_POINT('Origin',(-1.55588456152528E-16,7.49274514625042E-17,
-1.08333333333333));
#40746=CARTESIAN_POINT('Origin',(-1.55588456152528E-16,7.49274514625042E-17,
-1.08333333333333));
#40747=CARTESIAN_POINT('Origin',(1.55588456152528E-16,-7.49274514625042E-17,
1.08333333333333));
#40748=CARTESIAN_POINT('Origin',(1.55588456152528E-16,-7.49274514625042E-17,
1.08333333333333));
#40749=CARTESIAN_POINT('Origin',(1.55588456152528E-16,-7.49274514625042E-17,
1.08333333333333));
#40750=CARTESIAN_POINT('Origin',(1.55588456152528E-16,-7.49274514625042E-17,
1.08333333333333));
#40751=CARTESIAN_POINT('Origin',(1.55588456152528E-16,-7.49274514625042E-17,
1.08333333333333));
#40752=CARTESIAN_POINT('Origin',(1.94015631396094E-16,-2.43287906657286E-16,
1.08333333333333));
#40753=CARTESIAN_POINT('Origin',(1.94015631396094E-16,-2.43287906657286E-16,
1.08333333333333));
#40754=CARTESIAN_POINT('Origin',(-1.94015631396094E-16,2.43287906657286E-16,
-1.08333333333333));
#40755=CARTESIAN_POINT('Origin',(1.94015631396094E-16,-2.43287906657286E-16,
1.08333333333333));
#40756=CARTESIAN_POINT('Origin',(-1.94015631396094E-16,2.43287906657286E-16,
-1.08333333333333));
#40757=CARTESIAN_POINT('Origin',(1.94015631396094E-16,-2.43287906657286E-16,
1.08333333333333));
#40758=CARTESIAN_POINT('Origin',(-1.94015631396094E-16,2.43287906657286E-16,
-1.08333333333333));
#40759=CARTESIAN_POINT('Origin',(1.94015631396094E-16,-2.43287906657286E-16,
1.08333333333333));
#40760=CARTESIAN_POINT('Origin',(13.0227870731057,-2.97236616780865,3.45272288248773));
#40761=CARTESIAN_POINT('Origin',(14.7626584240763,-3.36948044994605,3.45272288248773));
#40762=CARTESIAN_POINT('Origin',(-1.94015631396094E-16,2.43287906657286E-16,
-1.08333333333333));
#40763=CARTESIAN_POINT('Origin',(-1.94015631396094E-16,2.43287906657286E-16,
-1.08333333333333));
#40764=CARTESIAN_POINT('Origin',(-1.94015631396094E-16,2.43287906657286E-16,
-1.08333333333333));
#40765=CARTESIAN_POINT('Origin',(1.94015631396094E-16,-2.43287906657286E-16,
1.08333333333333));
#40766=CARTESIAN_POINT('Origin',(1.94015631396094E-16,-2.43287906657286E-16,
1.08333333333333));
#40767=CARTESIAN_POINT('Origin',(1.94015631396094E-16,-2.43287906657286E-16,
1.08333333333333));
#40768=CARTESIAN_POINT('Origin',(1.94015631396094E-16,-2.43287906657286E-16,
1.08333333333333));
#40769=CARTESIAN_POINT('Origin',(1.94015631396094E-16,-2.43287906657286E-16,
1.08333333333333));
#40770=CARTESIAN_POINT('Origin',(8.63450790007668E-17,-3.78302508895262E-16,
1.08333333333333));
#40771=CARTESIAN_POINT('Origin',(8.63450790007668E-17,-3.78302508895262E-16,
1.08333333333333));
#40772=CARTESIAN_POINT('Origin',(-8.63450790007668E-17,3.78302508895262E-16,
-1.08333333333333));
#40773=CARTESIAN_POINT('Origin',(8.63450790007668E-17,-3.78302508895262E-16,
1.08333333333333));
#40774=CARTESIAN_POINT('Origin',(-8.63450790007668E-17,3.78302508895262E-16,
-1.08333333333333));
#40775=CARTESIAN_POINT('Origin',(8.63450790007668E-17,-3.78302508895262E-16,
1.08333333333333));
#40776=CARTESIAN_POINT('Origin',(-8.63450790007668E-17,3.78302508895262E-16,
-1.08333333333333));
#40777=CARTESIAN_POINT('Origin',(8.63450790007668E-17,-3.78302508895262E-16,
1.08333333333333));
#40778=CARTESIAN_POINT('Origin',(5.79568548444348,-12.0348649162504,3.45272288248773));
#40779=CARTESIAN_POINT('Origin',(6.57000108040713,-13.6427478189685,3.45272288248772));
#40780=CARTESIAN_POINT('Origin',(-8.63450790007668E-17,3.78302508895262E-16,
-1.08333333333333));
#40781=CARTESIAN_POINT('Origin',(-8.63450790007668E-17,3.78302508895262E-16,
-1.08333333333333));
#40782=CARTESIAN_POINT('Origin',(-8.63450790007668E-17,3.78302508895262E-16,
-1.08333333333333));
#40783=CARTESIAN_POINT('Origin',(8.63450790007668E-17,-3.78302508895262E-16,
1.08333333333333));
#40784=CARTESIAN_POINT('Origin',(8.63450790007668E-17,-3.78302508895262E-16,
1.08333333333333));
#40785=CARTESIAN_POINT('Origin',(8.63450790007668E-17,-3.78302508895262E-16,
1.08333333333333));
#40786=CARTESIAN_POINT('Origin',(8.63450790007668E-17,-3.78302508895262E-16,
1.08333333333333));
#40787=CARTESIAN_POINT('Origin',(8.63450790007668E-17,-3.78302508895262E-16,
1.08333333333333));
#40788=CARTESIAN_POINT('Origin',(-8.63450790007644E-17,-3.78302508895264E-16,
1.08333333333333));
#40789=CARTESIAN_POINT('Origin',(-8.63450790007644E-17,-3.78302508895264E-16,
1.08333333333333));
#40790=CARTESIAN_POINT('Origin',(8.63450790007644E-17,3.78302508895264E-16,
-1.08333333333333));
#40791=CARTESIAN_POINT('Origin',(-8.63450790007644E-17,-3.78302508895264E-16,
1.08333333333333));
#40792=CARTESIAN_POINT('Origin',(8.63450790007644E-17,3.78302508895264E-16,
-1.08333333333333));
#40793=CARTESIAN_POINT('Origin',(-8.63450790007644E-17,-3.78302508895264E-16,
1.08333333333333));
#40794=CARTESIAN_POINT('Origin',(8.63450790007644E-17,3.78302508895264E-16,
-1.08333333333333));
#40795=CARTESIAN_POINT('Origin',(-8.63450790007644E-17,-3.78302508895264E-16,
1.08333333333333));
#40796=CARTESIAN_POINT('Origin',(-5.79568548444331,-12.0348649162504,3.45272288248773));
#40797=CARTESIAN_POINT('Origin',(-6.57000108040694,-13.6427478189686,3.45272288248772));
#40798=CARTESIAN_POINT('Origin',(8.63450790007644E-17,3.78302508895264E-16,
-1.08333333333333));
#40799=CARTESIAN_POINT('Origin',(8.63450790007644E-17,3.78302508895264E-16,
-1.08333333333333));
#40800=CARTESIAN_POINT('Origin',(8.63450790007644E-17,3.78302508895264E-16,
-1.08333333333333));
#40801=CARTESIAN_POINT('Origin',(-8.63450790007644E-17,-3.78302508895264E-16,
1.08333333333333));
#40802=CARTESIAN_POINT('Origin',(-8.63450790007644E-17,-3.78302508895264E-16,
1.08333333333333));
#40803=CARTESIAN_POINT('Origin',(-8.63450790007644E-17,-3.78302508895264E-16,
1.08333333333333));
#40804=CARTESIAN_POINT('Origin',(-8.63450790007644E-17,-3.78302508895264E-16,
1.08333333333333));
#40805=CARTESIAN_POINT('Origin',(-8.63450790007644E-17,-3.78302508895264E-16,
1.08333333333333));
#40806=CARTESIAN_POINT('Origin',(-1.94015631396093E-16,-2.43287906657289E-16,
1.08333333333333));
#40807=CARTESIAN_POINT('Origin',(-1.94015631396093E-16,-2.43287906657289E-16,
1.08333333333333));
#40808=CARTESIAN_POINT('Origin',(1.94015631396093E-16,2.43287906657289E-16,
-1.08333333333333));
#40809=CARTESIAN_POINT('Origin',(-1.94015631396093E-16,-2.43287906657289E-16,
1.08333333333333));
#40810=CARTESIAN_POINT('Origin',(1.94015631396093E-16,2.43287906657289E-16,
-1.08333333333333));
#40811=CARTESIAN_POINT('Origin',(-1.94015631396093E-16,-2.43287906657289E-16,
1.08333333333333));
#40812=CARTESIAN_POINT('Origin',(1.94015631396093E-16,2.43287906657289E-16,
-1.08333333333333));
#40813=CARTESIAN_POINT('Origin',(-1.94015631396093E-16,-2.43287906657289E-16,
1.08333333333333));
#40814=CARTESIAN_POINT('Origin',(-13.0227870731057,-2.97236616780882,3.45272288248773));
#40815=CARTESIAN_POINT('Origin',(-14.7626584240763,-3.36948044994625,3.45272288248773));
#40816=CARTESIAN_POINT('Origin',(1.94015631396093E-16,2.43287906657289E-16,
-1.08333333333333));
#40817=CARTESIAN_POINT('Origin',(1.94015631396093E-16,2.43287906657289E-16,
-1.08333333333333));
#40818=CARTESIAN_POINT('Origin',(1.94015631396093E-16,2.43287906657289E-16,
-1.08333333333333));
#40819=CARTESIAN_POINT('Origin',(-1.94015631396093E-16,-2.43287906657289E-16,
1.08333333333333));
#40820=CARTESIAN_POINT('Origin',(-1.94015631396093E-16,-2.43287906657289E-16,
1.08333333333333));
#40821=CARTESIAN_POINT('Origin',(-1.94015631396093E-16,-2.43287906657289E-16,
1.08333333333333));
#40822=CARTESIAN_POINT('Origin',(-1.94015631396093E-16,-2.43287906657289E-16,
1.08333333333333));
#40823=CARTESIAN_POINT('Origin',(-1.94015631396093E-16,-2.43287906657289E-16,
1.08333333333333));
#40824=CARTESIAN_POINT('Origin',(-1.55588456152529E-16,-7.49274514625064E-17,
1.08333333333333));
#40825=CARTESIAN_POINT('Origin',(-1.55588456152529E-16,-7.49274514625064E-17,
1.08333333333333));
#40826=CARTESIAN_POINT('Origin',(1.55588456152529E-16,7.49274514625064E-17,
-1.08333333333333));
#40827=CARTESIAN_POINT('Origin',(-1.55588456152529E-16,-7.49274514625064E-17,
1.08333333333333));
#40828=CARTESIAN_POINT('Origin',(1.55588456152529E-16,7.49274514625064E-17,
-1.08333333333333));
#40829=CARTESIAN_POINT('Origin',(-1.55588456152529E-16,-7.49274514625064E-17,
1.08333333333333));
#40830=CARTESIAN_POINT('Origin',(1.55588456152529E-16,7.49274514625064E-17,
-1.08333333333333));
#40831=CARTESIAN_POINT('Origin',(-1.55588456152529E-16,-7.49274514625064E-17,
1.08333333333333));
#40832=CARTESIAN_POINT('Origin',(-10.4434643792749,8.32838493021299,3.45272288248773));
#40833=CARTESIAN_POINT('Origin',(-11.838732871064,9.44107442276088,3.45272288248773));
#40834=CARTESIAN_POINT('Origin',(1.55588456152529E-16,7.49274514625064E-17,
-1.08333333333333));
#40835=CARTESIAN_POINT('Origin',(1.55588456152529E-16,7.49274514625064E-17,
-1.08333333333333));
#40836=CARTESIAN_POINT('Origin',(1.55588456152529E-16,7.49274514625064E-17,
-1.08333333333333));
#40837=CARTESIAN_POINT('Origin',(-1.55588456152529E-16,-7.49274514625064E-17,
1.08333333333333));
#40838=CARTESIAN_POINT('Origin',(-1.55588456152529E-16,-7.49274514625064E-17,
1.08333333333333));
#40839=CARTESIAN_POINT('Origin',(-1.55588456152529E-16,-7.49274514625064E-17,
1.08333333333333));
#40840=CARTESIAN_POINT('Origin',(-1.55588456152529E-16,-7.49274514625064E-17,
1.08333333333333));
#40841=CARTESIAN_POINT('Origin',(-1.55588456152529E-16,-7.49274514625064E-17,
1.08333333333333));
#40842=CARTESIAN_POINT('Origin',(0.,0.,1.08333333333333));
#40843=CARTESIAN_POINT('Origin',(0.,0.,1.08333333333333));
#40844=CARTESIAN_POINT('Origin',(0.,0.,1.08333333333333));
#40845=CARTESIAN_POINT('Origin',(0.,0.,-1.08333333333333));
#40846=CARTESIAN_POINT('Origin',(0.,0.,-1.08333333333333));
#40847=CARTESIAN_POINT('Origin',(0.,0.,-1.08333333333333));
#40848=CARTESIAN_POINT('Origin',(0.,0.,1.08333333333333));
#40849=CARTESIAN_POINT('Origin',(0.,0.,1.08333333333333));
#43766=UNCERTAINTY_MEASURE_WITH_UNIT(LENGTH_MEASURE(0.01),#43782,
'DISTANCE_ACCURACY_VALUE',
'Maximum model space distance between geometric entities at asserted c
onnectivities');
#43771=UNCERTAINTY_MEASURE_WITH_UNIT(LENGTH_MEASURE(0.01),#43782,
'DISTANCE_ACCURACY_VALUE',
'Maximum model space distance between geometric entities at asserted c
onnectivities');
#43776=(
GEOMETRIC_REPRESENTATION_CONTEXT(3)
GLOBAL_UNCERTAINTY_ASSIGNED_CONTEXT((#43766))
GLOBAL_UNIT_ASSIGNED_CONTEXT((#43782,#43784,#43785))
REPRESENTATION_CONTEXT('','3D')
);
#43781=(
GEOMETRIC_REPRESENTATION_CONTEXT(3)
GLOBAL_UNCERTAINTY_ASSIGNED_CONTEXT((#43771))
GLOBAL_UNIT_ASSIGNED_CONTEXT((#43782,#43784,#43785))
REPRESENTATION_CONTEXT('','3D')
);
#43782=(
LENGTH_UNIT()
NAMED_UNIT(*)
SI_UNIT(.MILLI.,.METRE.)
);
#43784=(
NAMED_UNIT(*)
PLANE_ANGLE_UNIT()
SI_UNIT($,.RADIAN.)
);
#43785=(
NAMED_UNIT(*)
SI_UNIT($,.STERADIAN.)
SOLID_ANGLE_UNIT()
);
#43790=SHAPE_DEFINITION_REPRESENTATION(#43799,#43816);
#43799=PRODUCT_DEFINITION_SHAPE('',$,#43826);
#43816=SHAPE_REPRESENTATION('',(#13940),#43776);
#43821=PRODUCT_DEFINITION_CONTEXT('part definition',#43850,'design');
#43826=PRODUCT_DEFINITION('5972K117_Steel Ball Bearing_1','Bearing_02',
#43835,#43821);
#43835=PRODUCT_DEFINITION_FORMATION('',$,#43856);
#43850=APPLICATION_CONTEXT(
'Core Data for Automotive Mechanical Design Process');
#43851=PRODUCT_CONTEXT('part definition',#43850,'mechanical');
#43856=PRODUCT('5972K117_Steel Ball Bearing_1','Bearing_02',$,(#43851));
#43863=PRESENTATION_STYLE_ASSIGNMENT((#43866));
#43866=SURFACE_STYLE_USAGE(.BOTH.,#43869);
#43869=SURFACE_SIDE_STYLE('',(#43872));
#43872=SURFACE_STYLE_FILL_AREA(#43875);
#43875=FILL_AREA_STYLE('Opaque(160,160,160)',(#43878));
#43878=FILL_AREA_STYLE_COLOUR('Opaque(160,160,160)',#43881);
#43881=COLOUR_RGB('Opaque(160,160,160)', 0.31764706, 0.68627451, 0.89019608);
ENDSEC;
END-ISO-10303-21;
